ISO-10303-21;
HEADER;
FILE_DESCRIPTION (('STEP AP203'),
    '1' );
FILE_NAME ('ShearsLockingLatch_Predeterminado.step',
    '2026-10-08T11:28:20',
    ( '' ),
    ( '' ),
    'SwSTEP 2.0',
    'SolidWorks 2024',
    '' );
FILE_SCHEMA (( 'AUTOMOTIVE_DESIGN' ));
ENDSEC;

DATA;
#11=AXIS2_PLACEMENT_3D ( 'NONE', #1949, #8982, #6882 ) ;
#28=CIRCLE ( 'NONE', #12604, 8.192786906463668473 ) ;
#50=DIRECTION ( 'NONE',  ( 0.000000000000000000, 0.000000000000000000, 1.000000000000000000 ) ) ;
#51=CARTESIAN_POINT ( 'NONE',  ( -9.030574454602202650, -2.490287375297125294, -34.97919997656153157 ) ) ;
#173=CARTESIAN_POINT ( 'NONE',  ( -10.72138378296756756, -1.921202954650397476, -40.62330995231929620 ) ) ;
#190=ORIENTED_EDGE ( 'NONE', *, *, #14252, .F. ) ;
#203=ORIENTED_EDGE ( 'NONE', *, *, #9865, .F. ) ;
#213=CARTESIAN_POINT ( 'NONE',  ( -9.030574454602195544, -2.490287375297125294, -34.97919997656152447 ) ) ;
#219=EDGE_CURVE ( 'NONE', #9239, #1748, #2967, .T. ) ;
#232=( BOUNDED_SURFACE ( )  B_SPLINE_SURFACE ( 3, 1, ( 
 ( #3931, #529 ),
 ( #12031, #14691 ),
 ( #8632, #9877 ),
 ( #298, #8796 ) ),
 .UNSPECIFIED., .F., .F., .T. ) 
 B_SPLINE_SURFACE_WITH_KNOTS ( ( 4, 4 ),
 ( 2, 2 ),
 ( 0.000000000000000000, 1.000000000000000000 ),
 ( 0.000000000000000000, 1.000000000000000000 ),
 .UNSPECIFIED. ) 
 GEOMETRIC_REPRESENTATION_ITEM ( )  RATIONAL_B_SPLINE_SURFACE ( (
 ( 1.000000000000000000, 1.000000000000000000),
 ( 0.6468719831415908894, 0.6468719831415908894),
 ( 0.6468719831415908894, 0.6468719831415908894),
 ( 1.000000000000000000, 1.000000000000000000) ) ) 
 REPRESENTATION_ITEM ( '' )  SURFACE ( )  );
#243=EDGE_LOOP ( 'NONE', ( #11028, #10928, #1338, #8785, #9085 ) ) ;
#245=CARTESIAN_POINT ( 'NONE',  ( -9.836272398077410273, -1.921202954650397032, -34.71741284551207229 ) ) ;
#267=ORIENTED_EDGE ( 'NONE', *, *, #4780, .T. ) ;
#298=CARTESIAN_POINT ( 'NONE',  ( -8.289881740238500996, 2.075239479414269894, -35.21986562831451550 ) ) ;
#299=CARTESIAN_POINT ( 'NONE',  ( 4.554677347145018373, -2.225540348348185052E-17, -1.000000000000000000 ) ) ;
#329=CARTESIAN_POINT ( 'NONE',  ( -6.119281984250456219, -2.490287375297126626, -44.38286699775952826 ) ) ;
#338=DIRECTION ( 'NONE',  ( -0.9510565162951488682, 0.000000000000000000, 0.3090169943749619952 ) ) ;
#375=CARTESIAN_POINT ( 'NONE',  ( -3.616507224213203475, 2.490287375297124850, -0.7961248001406434627 ) ) ;
#380=MECHANICAL_CONTEXT ( 'NONE', #1665, 'mechanical' ) ;
#399=LINE ( 'NONE', #5948, #9300 ) ;
#407=CARTESIAN_POINT ( 'NONE',  ( 7.148068729939689447, -2.490287375297126626, -34.56909192082981974 ) ) ;
#433=ADVANCED_FACE ( 'NONE', ( #13637 ), #3589, .F. ) ;
#448=CARTESIAN_POINT ( 'NONE',  ( -4.878690035801932723, 1.020558061026469066, -0.3860167444088121180 ) ) ;
#492=CARTESIAN_POINT ( 'NONE',  ( -0.7011654427748897911, 2.490287375297123962, -44.24552462515097773 ) ) ;
#505=VERTEX_POINT ( 'NONE', #10446 ) ;
#522=CARTESIAN_POINT ( 'NONE',  ( -4.422205167688408878, 1.921202954650395256, -0.5343376690911894045 ) ) ;
#524=CARTESIAN_POINT ( 'NONE',  ( -5.445322652854981627, 5.900679960901947346E-16, -1.000000000000000000 ) ) ;
#529=CARTESIAN_POINT ( 'NONE',  ( -3.578160823487617215, 2.490287375297123518, -0.5540151544771234615 ) ) ;
#575=FACE_OUTER_BOUND ( 'NONE', #10280, .T. ) ;
#603=CARTESIAN_POINT ( 'NONE',  ( -9.030574454602195544, 2.490287375297124850, -34.97919997656152447 ) ) ;
#630=CARTESIAN_POINT ( 'NONE',  ( 7.352489943804302541, -2.075239479414269894, -39.38380306805898101 ) ) ;
#634=UNCERTAINTY_MEASURE_WITH_UNIT (LENGTH_MEASURE( 1.000000000000000082E-05 ), #8357, 'distance_accuracy_value', 'NONE');
#639=CARTESIAN_POINT ( 'NONE',  ( 1.831246893856136593, -2.490287375297125294, -1.000000000000021760 ) ) ;
#644=CARTESIAN_POINT ( 'NONE',  ( 3.554677347145018373, -2.225540348348185052E-17, 1.000000000000000000 ) ) ;
#647=EDGE_CURVE ( 'NONE', #6217, #2052, #399, .T. ) ;
#649=CARTESIAN_POINT ( 'NONE',  ( 3.158384440324541131, 1.020558061026468177, -1.000000000000027311 ) ) ;
#651=CARTESIAN_POINT ( 'NONE',  ( -8.289881740238515206, 2.529993217055222843, -35.21986562831452261 ) ) ;
#689=DIRECTION ( 'NONE',  ( 0.000000000000000000, 0.000000000000000000, 1.000000000000000000 ) ) ;
#701=CARTESIAN_POINT ( 'NONE',  ( 8.475206276408092876, 0.000000000000000000, -34.56909192082981974 ) ) ;
#708=EDGE_CURVE ( 'NONE', #8297, #505, #6593, .T. ) ;
#720=CARTESIAN_POINT ( 'NONE',  ( 1.488703080326642114, 2.579293035051159144, -1.000000000000001332 ) ) ;
#722=CARTESIAN_POINT ( 'NONE',  ( 6.770579566034212071, 2.743867526398027223, -34.56909192082981974 ) ) ;
#726=DIRECTION ( 'NONE',  ( -0.1564344650402312298, 0.000000000000000000, 0.9876883405951376593 ) ) ;
#761=CARTESIAN_POINT ( 'NONE',  ( -4.509114193367754986, 1.625551886426498394, -1.000000000000011768 ) ) ;
#769=CIRCLE ( 'NONE', #2753, 8.192786906463668473 ) ;
#790=CARTESIAN_POINT ( 'NONE',  ( 3.158384440324539355, 0.000000000000000000, -1.000000000000021760 ) ) ;
#803=CARTESIAN_POINT ( 'NONE',  ( 4.529353718053122257, 2.743867526398027223, -43.69627513258503626 ) ) ;
#814=VERTEX_POINT ( 'NONE', #6103 ) ;
#820=CARTESIAN_POINT ( 'NONE',  ( -9.030574454602195544, -2.490287375297125294, -34.97919997656152447 ) ) ;
#860=CARTESIAN_POINT ( 'NONE',  ( 1.052436484934206051, -2.529993217055220178, -1.000000000000021760 ) ) ;
#873=CARTESIAN_POINT ( 'NONE',  ( 1.831246893856137481, 2.490287375297123074, -1.000000000000007772 ) ) ;
#903=FACE_OUTER_BOUND ( 'NONE', #9111, .T. ) ;
#923=CARTESIAN_POINT ( 'NONE',  ( -4.364759770003678874, -1.831210392890419758, -1.000000000000001332 ) ) ;
#934=CYLINDRICAL_SURFACE ( 'NONE', #12406, 5.000000000000000000 ) ;
#943=CARTESIAN_POINT ( 'NONE',  ( 1.170341033097332506, 2.410101856083639138, -1.000000000000001110 ) ) ;
#978=CARTESIAN_POINT ( 'NONE',  ( -0.4453226528549816265, -2.225540348348185052E-17, -1.000000000000000000 ) ) ;
#1018=CARTESIAN_POINT ( 'NONE',  ( 1.077441151898745231, 2.255542499959171554, -1.000000000000001776 ) ) ;
#1034=AXIS2_PLACEMENT_3D ( 'NONE', #978, #50, #11786 ) ;
#1066=CARTESIAN_POINT ( 'NONE',  ( 8.475206276408092876, 1.020558061026469510, -34.56909192082981974 ) ) ;
#1089=CARTESIAN_POINT ( 'NONE',  ( -8.289881740238502772, -2.075239479414269894, -35.21986562831451550 ) ) ;
#1121=CARTESIAN_POINT ( 'NONE',  ( 2.035195838443857763, -2.353283696435568118, -1.000000000000001110 ) ) ;
#1141=CARTESIAN_POINT ( 'NONE',  ( -0.8336906130587268260, 1.921202954650395700, -45.08225561976306039 ) ) ;
#1145=CARTESIAN_POINT ( 'NONE',  ( -4.975935430107378821, 0.000000000000000000, -1.000000000000001332 ) ) ;
#1147=PLANE ( 'NONE',  #7230 ) ;
#1202=CARTESIAN_POINT ( 'NONE',  ( -6.119281984250456219, -2.490287375297125294, -44.38286699775952826 ) ) ;
#1207=CARTESIAN_POINT ( 'NONE',  ( -10.29275726619094300, 0.000000000000000000, -34.56909192082969895 ) ) ;
#1272=ORIENTED_EDGE ( 'NONE', *, *, #2054, .T. ) ;
#1292=EDGE_CURVE ( 'NONE', #814, #12909, #2740, .T. ) ;
#1333=CARTESIAN_POINT ( 'NONE',  ( 8.475206276408092876, -1.020558061026470176, -34.56909192082981974 ) ) ;
#1338=ORIENTED_EDGE ( 'NONE', *, *, #11568, .F. ) ;
#1349=LINE ( 'NONE', #4826, #1358 ) ;
#1351=ORIENTED_EDGE ( 'NONE', *, *, #8138, .T. ) ;
#1358=VECTOR ( 'NONE', #3512, 1000.000000000000227 ) ;
#1384=EDGE_CURVE ( 'NONE', #13806, #12909, #13290, .T. ) ;
#1404=VERTEX_POINT ( 'NONE', #3775 ) ;
#1409=CARTESIAN_POINT ( 'NONE',  ( -9.030574454602202650, -2.490287375297126626, -34.97919997656153157 ) ) ;
#1480=CARTESIAN_POINT ( 'NONE',  ( -7.194037649453649763, 0.000000000000000000, -45.55632290616381397 ) ) ;
#1521=B_SPLINE_CURVE_WITH_KNOTS ( 'NONE', 3,
 ( #14049, #3446, #8160, #11789, #3607, #5911, #8309, #8384, #13037, #11863 ),
 .UNSPECIFIED., .F., .F.,
 ( 4, 2, 2, 2, 4 ),
 ( 0.000000000000000000, 0.0007311508082448065502, 0.001462301616489612667, 0.002193452424734418892, 0.002924603232979224900 ),
 .UNSPECIFIED. ) ;
#1551=CARTESIAN_POINT ( 'NONE',  ( 4.329912723285513465, -2.075239479414269894, -43.25836301743400725 ) ) ;
#1578=VERTEX_POINT ( 'NONE', #213 ) ;
#1581=VECTOR ( 'NONE', #3087, 1000.000000000000114 ) ;
#1597=DIRECTION ( 'NONE',  ( 0.000000000000000000, 0.000000000000000000, 1.000000000000000000 ) ) ;
#1604=EDGE_CURVE ( 'NONE', #1578, #13029, #5211, .T. ) ;
#1665=APPLICATION_CONTEXT ( 'configuration controlled 3d designs of mechanical parts and assemblies' ) ;
#1717=CARTESIAN_POINT ( 'NONE',  ( 2.678407845566782353, 1.921202954650393924, -1.000000000000027311 ) ) ;
#1748=VERTEX_POINT ( 'NONE', #3004 ) ;
#1770=LINE ( 'NONE', #12204, #2053 ) ;
#1803=CARTESIAN_POINT ( 'NONE',  ( -8.289881740238502772, -2.075239479414269894, -35.21986562831451550 ) ) ;
#1806=CARTESIAN_POINT ( 'NONE',  ( 4.329912723285513465, 2.075239479414269894, -43.25836301743400725 ) ) ;
#1821=CARTESIAN_POINT ( 'NONE',  ( 6.369258321017759350, -2.075239479414269894, -34.56909192082981974 ) ) ;
#1825=AXIS2_PLACEMENT_3D ( 'NONE', #13079, #2727, #2494 ) ;
#1845=CARTESIAN_POINT ( 'NONE',  ( -4.738306685235110116, 1.195290186917868924, -1.000000000000011768 ) ) ;
#1884=CARTESIAN_POINT ( 'NONE',  ( -9.030574454602209755, 2.490287375297123962, -34.97919997656153157 ) ) ;
#1917=CARTESIAN_POINT ( 'NONE',  ( -4.975935430107380597, 0.2459835157955775065, -1.000000000000011990 ) ) ;
#1932=CARTESIAN_POINT ( 'NONE',  ( 7.753811188820753486, -2.743867526398026335, -39.64929316069592602 ) ) ;
#1949=CARTESIAN_POINT ( 'NONE',  ( -0.9087754948914270603, 0.000000000000000000, -36.05536862169275025 ) ) ;
#1984=AXIS2_PLACEMENT_3D ( 'NONE', #9301, #8356, #6206 ) ;
#2003=CARTESIAN_POINT ( 'NONE',  ( -2.894992141681591136, 2.255542499959168001, -1.000000000000001332 ) ) ;
#2009=CARTESIAN_POINT ( 'NONE',  ( -0.7011654427748897911, -2.490287375297125294, -44.24552462515097062 ) ) ;
#2013=EDGE_LOOP ( 'NONE', ( #7617, #7244, #3186, #12149 ) ) ;
#2045=CARTESIAN_POINT ( 'NONE',  ( -3.305084003370867052, -2.579141538380387733, -1.000000000000001110 ) ) ;
#2052=VERTEX_POINT ( 'NONE', #8411 ) ;
#2053=VECTOR ( 'NONE', #8876, 1000.000000000000114 ) ;
#2054=EDGE_CURVE ( 'NONE', #12985, #12117, #3555, .T. ) ;
#2069=FACE_BOUND ( 'NONE', #243, .T. ) ;
#2087=ORIENTED_EDGE ( 'NONE', *, *, #5451, .T. ) ;
#2093=CARTESIAN_POINT ( 'NONE',  ( 1.169562822776721855, -2.409215066305258279, -1.000000000000001332 ) ) ;
#2113=ORIENTED_EDGE ( 'NONE', *, *, #13782, .F. ) ;
#2158=EDGE_CURVE ( 'NONE', #12985, #5655, #10819, .T. ) ;
#2160=CARTESIAN_POINT ( 'NONE',  ( -3.648797883638980277, -2.490287375297125294, -1.000000000000000888 ) ) ;
#2228=CARTESIAN_POINT ( 'NONE',  ( -4.036619102201398412, -2.193945312325716657, -1.000000000000001110 ) ) ;
#2231=FACE_OUTER_BOUND ( 'NONE', #5069, .T. ) ;
#2246=CIRCLE ( 'NONE', #13847, 5.000000000000000000 ) ;
#2256=AXIS2_PLACEMENT_3D ( 'NONE', #9939, #1597, #4079 ) ;
#2297=CARTESIAN_POINT ( 'NONE',  ( -5.813579972774820526, -2.743867526398026335, -44.04909082593601966 ) ) ;
#2300=ORIENTED_EDGE ( 'NONE', *, *, #5832, .F. ) ;
#2302=FACE_OUTER_BOUND ( 'NONE', #12938, .T. ) ;
#2311=MANIFOLD_SOLID_BREP ( 'Redondeo1', #11529 ) ;
#2314=VECTOR ( 'NONE', #2596, 1000.000000000000000 ) ;
#2320=( BOUNDED_SURFACE ( )  B_SPLINE_SURFACE ( 3, 1, ( 
 ( #11721, #9482 ),
 ( #7470, #448 ),
 ( #11101, #522 ),
 ( #603, #375 ) ),
 .UNSPECIFIED., .F., .F., .F. ) 
 B_SPLINE_SURFACE_WITH_KNOTS ( ( 4, 4 ),
 ( 2, 2 ),
 ( 0.000000000000000000, 1.000000000000000000 ),
 ( 0.000000000000000000, 1.000000000000000000 ),
 .UNSPECIFIED. ) 
 GEOMETRIC_REPRESENTATION_ITEM ( )  RATIONAL_B_SPLINE_SURFACE ( (
 ( 1.000000000000000000, 1.000000000000000000),
 ( 0.9216682375510407699, 0.9216682375510407699),
 ( 0.9216682375510407699, 0.9216682375510407699),
 ( 1.000000000000000000, 1.000000000000000000) ) ) 
 REPRESENTATION_ITEM ( '' )  SURFACE ( )  );
#2323=ORIENTED_EDGE ( 'NONE', *, *, #4424, .T. ) ;
#2338=AXIS2_PLACEMENT_3D ( 'NONE', #3259, #12540, #6438 ) ;
#2384=DIRECTION ( 'NONE',  ( 1.000000000000000000, 0.000000000000000000, 0.000000000000000000 ) ) ;
#2409=ORIENTED_EDGE ( 'NONE', *, *, #5347, .T. ) ;
#2427=DIRECTION ( 'NONE',  ( -0.3090169943749621062, 0.000000000000000000, -0.9510565162951489793 ) ) ;
#2436=ADVANCED_FACE ( 'NONE', ( #5562 ), #10494, .T. ) ;
#2474=AXIS2_PLACEMENT_3D ( 'NONE', #13489, #5052, #338 ) ;
#2491=CARTESIAN_POINT ( 'NONE',  ( -0.7011654427748897911, -2.490287375297126626, -44.24552462515097062 ) ) ;
#2494=DIRECTION ( 'NONE',  ( -1.000000000000000000, 1.224646799147353454E-16, 0.000000000000000000 ) ) ;
#2495=ORIENTED_EDGE ( 'NONE', *, *, #4220, .F. ) ;
#2510=DIRECTION ( 'NONE',  ( -0.9510565162951475360, 0.000000000000000000, 0.3090169943749664916 ) ) ;
#2525=EDGE_CURVE ( 'NONE', #12117, #1578, #7925, .T. ) ;
#2558=AXIS2_PLACEMENT_3D ( 'NONE', #6039, #4884, #9595 ) ;
#2571=CARTESIAN_POINT ( 'NONE',  ( 9.458437899194636955, -1.020558061026470176, -40.77697206847473410 ) ) ;
#2586=CARTESIAN_POINT ( 'NONE',  ( -0.4453226528549816265, -2.225540348348185052E-17, 2.000000000000000000 ) ) ;
#2596=DIRECTION ( 'NONE',  ( 0.000000000000000000, 1.000000000000000000, -0.000000000000000000 ) ) ;
#2607=CARTESIAN_POINT ( 'NONE',  ( -11.27598888897756346, 0.000000000000000000, -40.77697206847459910 ) ) ;
#2647=CARTESIAN_POINT ( 'NONE',  ( 5.376486659670670853, 0.000000000000000000, -45.55632290616389923 ) ) ;
#2666=ORIENTED_EDGE ( 'NONE', *, *, #9993, .T. ) ;
#2727=DIRECTION ( 'NONE',  ( 1.224646799147353207E-16, 1.000000000000000000, -0.000000000000000000 ) ) ;
#2740=CIRCLE ( 'NONE', #12358, 5.000000000000000000 ) ;
#2753=AXIS2_PLACEMENT_3D ( 'NONE', #7559, #4248, #8720 ) ;
#2785=FACE_OUTER_BOUND ( 'NONE', #12166, .T. ) ;
#2793=CARTESIAN_POINT ( 'NONE',  ( 7.352489943804306094, -2.529993217055220178, -39.38380306805897391 ) ) ;
#2883=ORIENTED_EDGE ( 'NONE', *, *, #13980, .T. ) ;
#2890=CARTESIAN_POINT ( 'NONE',  ( 8.131300352726237080, 2.490287375297123962, -39.89901737624450107 ) ) ;
#2894=DIRECTION ( 'NONE',  ( 1.000000000000000000, 0.000000000000000000, 0.000000000000000000 ) ) ;
#2904=FACE_OUTER_BOUND ( 'NONE', #15245, .T. ) ;
#2912=ADVANCED_FACE ( 'NONE', ( #11011 ), #14581, .T. ) ;
#2937=CARTESIAN_POINT ( 'NONE',  ( -3.648797883638982054, 2.490287375297123962, -1.000000000000000888 ) ) ;
#2959=CARTESIAN_POINT ( 'NONE',  ( -5.488578029460351893, 2.075239479414269894, -43.69424231201529096 ) ) ;
#2967=LINE ( 'NONE', #7598, #14009 ) ;
#2984=PRODUCT_DEFINITION ( 'UNKNOWN', '', #8443, #8817 ) ;
#3004=CARTESIAN_POINT ( 'NONE',  ( 1.052436484934203387, 2.075239479414269894, -1.000000000000007772 ) ) ;
#3039=CARTESIAN_POINT ( 'NONE',  ( 4.329912723285513465, 2.529993217055222399, -43.25836301743401435 ) ) ;
#3073=CARTESIAN_POINT ( 'NONE',  ( -3.648797883638982054, 2.490287375297123962, -1.000000000000000888 ) ) ;
#3084=CARTESIAN_POINT ( 'NONE',  ( -2.869987474717050624, 2.075239479414269894, -1.000000000000000888 ) ) ;
#3087=DIRECTION ( 'NONE',  ( -0.1564344650402312298, -0.000000000000000000, 0.9876883405951376593 ) ) ;
#3089=CARTESIAN_POINT ( 'NONE',  ( -9.306320601523863090, -2.743867526398026335, -40.23124431751399044 ) ) ;
#3113=CARTESIAN_POINT ( 'NONE',  ( -8.289881740238502772, -2.075239479414269894, -35.21986562831451550 ) ) ;
#3125=DIRECTION ( 'NONE',  ( -0.1564344650402312298, -0.000000000000000000, 0.9876883405951376593 ) ) ;
#3179=CARTESIAN_POINT ( 'NONE',  ( 1.668807522230304041, 2.569799602646715808, -1.000000000000001110 ) ) ;
#3186=ORIENTED_EDGE ( 'NONE', *, *, #2525, .T. ) ;
#3208=CARTESIAN_POINT ( 'NONE',  ( -9.030574454602195544, -2.490287375297124406, -34.97919997656152447 ) ) ;
#3231=CARTESIAN_POINT ( 'NONE',  ( 6.369258321017759350, 2.075239479414269894, -34.56909192082981974 ) ) ;
#3241=CARTESIAN_POINT ( 'NONE',  ( 6.369258321017760238, -2.529993217055220178, -34.56909192082981974 ) ) ;
#3253=DIRECTION ( 'NONE',  ( 0.000000000000000000, -1.000000000000000000, 0.000000000000000000 ) ) ;
#3259=CARTESIAN_POINT ( 'NONE',  ( -8.289881740238502772, -2.075239479414269894, -35.21986562831451550 ) ) ;
#3274=CARTESIAN_POINT ( 'NONE',  ( -2.987113812559607062, -2.409215066305300912, -1.000000000000001332 ) ) ;
#3285=ORIENTED_EDGE ( 'NONE', *, *, #12925, .F. ) ;
#3299=CIRCLE ( 'NONE', #1825, 1.000000000000000000 ) ;
#3312=CARTESIAN_POINT ( 'NONE',  ( 6.770579566034212071, 2.743867526398027223, -34.56909192082981974 ) ) ;
#3325=DIRECTION ( 'NONE',  ( 0.000000000000000000, 0.000000000000000000, 1.000000000000000000 ) ) ;
#3403=DIRECTION ( 'NONE',  ( 1.000000000000000000, 0.000000000000000000, 0.000000000000000000 ) ) ;
#3427=ORIENTED_EDGE ( 'NONE', *, *, #3454, .F. ) ;
#3432=EDGE_LOOP ( 'NONE', ( #10407, #1351, #13765, #12891 ) ) ;
#3444=CARTESIAN_POINT ( 'NONE',  ( 4.716951098700676859, -2.490287375297125294, -44.10818225254241298 ) ) ;
#3446=CARTESIAN_POINT ( 'NONE',  ( 2.036468110357356309, 2.352429041693352207, -1.000000000000007772 ) ) ;
#3454=EDGE_CURVE ( 'NONE', #505, #1748, #6689, .T. ) ;
#3463=AXIS2_PLACEMENT_3D ( 'NONE', #15028, #15182, #6662 ) ;
#3479=CARTESIAN_POINT ( 'NONE',  ( -5.445322652854981627, 5.900679960901947346E-16, -1.000000000000000000 ) ) ;
#3512=DIRECTION ( 'NONE',  ( 0.1564344650402314796, 0.000000000000000000, 0.9876883405951375483 ) ) ;
#3531=CARTESIAN_POINT ( 'NONE',  ( -9.030574454602202650, 2.490287375297125294, -34.97919997656153157 ) ) ;
#3555=LINE ( 'NONE', #1089, #3715 ) ;
#3567=ADVANCED_FACE ( 'NONE', ( #13334 ), #7910, .T. ) ;
#3574=ORIENTED_EDGE ( 'NONE', *, *, #5829, .F. ) ;
#3589=( BOUNDED_SURFACE ( )  B_SPLINE_SURFACE ( 3, 3, ( 
 ( #11075, #2890, #5426, #492, #14733, #12385, #1884 ),
 ( #722, #5286, #803, #9061, #10148, #6592, #6664 ),
 ( #14882, #8762, #3039, #12307, #4279, #6436, #651 ),
 ( #8984, #9998, #1806, #5504, #2959, #11380, #6363 ) ),
 .UNSPECIFIED., .F., .F., .F. ) 
 B_SPLINE_SURFACE_WITH_KNOTS ( ( 4, 4 ),
 ( 4, 3, 4 ),
 ( 0.000000000000000000, 1.000000000000000000 ),
 ( 0.000000000000000000, 0.5000000000000000000, 1.000000000000000000 ),
 .UNSPECIFIED. ) 
 GEOMETRIC_REPRESENTATION_ITEM ( )  RATIONAL_B_SPLINE_SURFACE ( (
 ( 1.000000000000000000, 0.7662986988867873661, 0.7662986988867873661, 1.000000000000000000, 0.7662986988867873661, 0.7662986988867873661, 1.000000000000000000),
 ( 0.6468719831415912225, 0.4956971590277172157, 0.4956971590277172157, 0.6468719831415912225, 0.4956971590277172157, 0.4956971590277172157, 0.6468719831415912225),
 ( 0.6468719831415912225, 0.4956971590277172157, 0.4956971590277172157, 0.6468719831415912225, 0.4956971590277172157, 0.4956971590277172157, 0.6468719831415912225),
 ( 1.000000000000000000, 0.7662986988867873661, 0.7662986988867873661, 1.000000000000000000, 0.7662986988867873661, 0.7662986988867873661, 1.000000000000000000) ) ) 
 REPRESENTATION_ITEM ( '' )  SURFACE ( )  );
#3607=CARTESIAN_POINT ( 'NONE',  ( 2.691563203584910635, 1.625551886426497727, -1.000000000000001110 ) ) ;
#3609=CARTESIAN_POINT ( 'NONE',  ( 5.137957026085652856, 1.921202954650395478, -45.03258396026100030 ) ) ;
#3611=DIRECTION ( 'NONE',  ( 1.000000000000000000, 0.000000000000000000, 0.000000000000000000 ) ) ;
#3650=VERTEX_POINT ( 'NONE', #524 ) ;
#3679=CARTESIAN_POINT ( 'NONE',  ( -10.72138378296757466, 1.921202954650395478, -40.62330995231931041 ) ) ;
#3691=ORIENTED_EDGE ( 'NONE', *, *, #6476, .F. ) ;
#3715=VECTOR ( 'NONE', #10663, 1000.000000000000000 ) ;
#3766=CARTESIAN_POINT ( 'NONE',  ( -0.9087754948914894548, 0.000000000000000000, -45.55632290616385660 ) ) ;
#3775=CARTESIAN_POINT ( 'NONE',  ( -3.648797883638982054, 2.490287375297123962, -1.000000000000000888 ) ) ;
#3875=DIRECTION ( 'NONE',  ( -0.1564344650402312298, -0.000000000000000000, 0.9876883405951376593 ) ) ;
#3889=DIRECTION ( 'NONE',  ( 1.000000000000000000, 0.000000000000000000, 0.000000000000000000 ) ) ;
#3890=ORIENTED_EDGE ( 'NONE', *, *, #11293, .T. ) ;
#3895=FACE_OUTER_BOUND ( 'NONE', #11410, .T. ) ;
#3931=CARTESIAN_POINT ( 'NONE',  ( -9.030574454602197321, 2.490287375297123518, -34.97919997656152447 ) ) ;
#3942=CARTESIAN_POINT ( 'NONE',  ( -0.4453226528549816265, -2.225540348348185052E-17, -1.000000000000000000 ) ) ;
#3950=AXIS2_PLACEMENT_3D ( 'NONE', #3982, #11305, #726 ) ;
#3951=CARTESIAN_POINT ( 'NONE',  ( -5.488578029460351893, -2.075239479414269894, -43.69424231201529096 ) ) ;
#3966=CARTESIAN_POINT ( 'NONE',  ( 3.158384440324536691, 0.000000000000000000, -1.000000000000001332 ) ) ;
#3982=CARTESIAN_POINT ( 'NONE',  ( 6.369258321017759350, -2.075239479414269894, -34.56909192082981974 ) ) ;
#4028=CARTESIAN_POINT ( 'NONE',  ( 8.475206276408092876, 0.000000000000000000, -34.56909192082981974 ) ) ;
#4036=CARTESIAN_POINT ( 'NONE',  ( -8.289881740238502772, 2.075239479414269894, -35.21986562831451550 ) ) ;
#4079=DIRECTION ( 'NONE',  ( 1.000000000000000000, 0.000000000000000000, 0.000000000000000000 ) ) ;
#4085=ORIENTED_EDGE ( 'NONE', *, *, #9243, .T. ) ;
#4086=CARTESIAN_POINT ( 'NONE',  ( -10.29275726619092524, 0.000000000000000000, -34.56909192082969184 ) ) ;
#4099=B_SPLINE_CURVE_WITH_KNOTS ( 'NONE', 3,
 ( #7911, #14750, #13877, #2045, #6757, #11471, #3274, #4148, #13574, #12861 ),
 .UNSPECIFIED., .F., .F.,
 ( 4, 2, 2, 2, 4 ),
 ( 9.697399036122160616E-19, 0.0002702708960404782783, 0.0005405417920809555809, 0.0008108126881214329377, 0.001081083584161910078 ),
 .UNSPECIFIED. ) ;
#4102=CARTESIAN_POINT ( 'NONE',  ( 7.148068729939693000, 2.490287375297123962, -34.56909192082981974 ) ) ;
#4107=CARTESIAN_POINT ( 'NONE',  ( -3.573755135669773875, 2.540697700118000224, -1.000000000001791012 ) ) ;
#4121=CARTESIAN_POINT ( 'NONE',  ( 8.475206276408092876, 0.000000000000000000, -34.56909192082981974 ) ) ;
#4148=CARTESIAN_POINT ( 'NONE',  ( -2.894564284656305553, -2.254417391461273734, -1.000000000000001110 ) ) ;
#4160=CARTESIAN_POINT ( 'NONE',  ( -0.9087754948914270603, 2.075239479414269894, -36.05536862169275025 ) ) ;
#4220=EDGE_CURVE ( 'NONE', #5312, #8297, #13602, .T. ) ;
#4247=ORIENTED_EDGE ( 'NONE', *, *, #4420, .T. ) ;
#4248=DIRECTION ( 'NONE',  ( 0.000000000000000000, 1.000000000000000000, 0.000000000000000000 ) ) ;
#4279=CARTESIAN_POINT ( 'NONE',  ( -5.488578029460351004, 2.529993217055222399, -43.69424231201528386 ) ) ;
#4336=ORIENTED_EDGE ( 'NONE', *, *, #14445, .F. ) ;
#4381=ORIENTED_EDGE ( 'NONE', *, *, #11293, .F. ) ;
#4394=SHAPE_REPRESENTATION ( 'ShearsLockingLatch_Predeterminado', ( #9419 ), #14368 ) ;
#4397=CARTESIAN_POINT ( 'NONE',  ( 1.052436484934207606, 2.529993217055222843, -1.000000000000029088 ) ) ;
#4404=CARTESIAN_POINT ( 'NONE',  ( 1.453757729950655886, -2.743867526398025447, -1.000000000000021760 ) ) ;
#4411=B_SPLINE_CURVE_WITH_KNOTS ( 'NONE', 3,
 ( #1145, #9486, #15234, #11796, #923, #2228, #8170, #2160 ),
 .UNSPECIFIED., .F., .F.,
 ( 4, 2, 2, 4 ),
 ( 0.002924603232979225333, 0.004377839289350649032, 0.005104457317536361532, 0.005831075345722074033 ),
 .UNSPECIFIED. ) ;
#4420=EDGE_CURVE ( 'NONE', #13029, #13794, #13087, .T. ) ;
#4424=EDGE_CURVE ( 'NONE', #12117, #9630, #9767, .T. ) ;
#4463=AXIS2_PLACEMENT_3D ( 'NONE', #7711, #12427, #689 ) ;
#4470=AXIS2_PLACEMENT_3D ( 'NONE', #644, #3253, #12378 ) ;
#4473=CARTESIAN_POINT ( 'NONE',  ( 6.369258321017759350, 2.529993217055222843, -34.56909192082981974 ) ) ;
#4516=ADVANCED_FACE ( 'NONE', ( #3895 ), #9404, .T. ) ;
#4540=AXIS2_PLACEMENT_3D ( 'NONE', #3942, #8644, #11199 ) ;
#4546=ORIENTED_EDGE ( 'NONE', *, *, #12925, .T. ) ;
#4566=CARTESIAN_POINT ( 'NONE',  ( 1.396221076823685792, -2.558678233169546790, -1.000000000000001332 ) ) ;
#4613=CARTESIAN_POINT ( 'NONE',  ( -4.975935430107378821, 0.000000000000000000, -1.000000000000001332 ) ) ;
#4669=ORIENTED_EDGE ( 'NONE', *, *, #13666, .T. ) ;
#4670=CARTESIAN_POINT ( 'NONE',  ( 2.689713740728195024, -1.628626824712336996, -1.000000000000001332 ) ) ;
#4683=CARTESIAN_POINT ( 'NONE',  ( 6.770579566034210295, -2.743867526398025447, -34.56909192082981974 ) ) ;
#4691=CARTESIAN_POINT ( 'NONE',  ( 8.131300352726233527, 2.490287375297125294, -39.89901737624450107 ) ) ;
#4694=EDGE_CURVE ( 'NONE', #5312, #13029, #7660, .T. ) ;
#4764=ORIENTED_EDGE ( 'NONE', *, *, #9993, .F. ) ;
#4765=EDGE_CURVE ( 'NONE', #13794, #12985, #6176, .T. ) ;
#4766=CARTESIAN_POINT ( 'NONE',  ( -7.194037649453649763, 0.000000000000000000, -45.55632290616381397 ) ) ;
#4779=VERTEX_POINT ( 'NONE', #13936 ) ;
#4780=EDGE_CURVE ( 'NONE', #1748, #10459, #6334, .T. ) ;
#4826=CARTESIAN_POINT ( 'NONE',  ( -10.29275726619092524, 0.000000000000000000, -34.56909192082969184 ) ) ;
#4843=CARTESIAN_POINT ( 'NONE',  ( -0.4453226528549816265, -2.225540348348185052E-17, 1.000000000000000000 ) ) ;
#4880=CARTESIAN_POINT ( 'NONE',  ( -10.29275726619094478, -1.020558061026470176, -34.56909192082969895 ) ) ;
#4884=DIRECTION ( 'NONE',  ( 0.000000000000000000, 1.000000000000000000, 0.000000000000000000 ) ) ;
#4901=ORIENTED_EDGE ( 'NONE', *, *, #13875, .F. ) ;
#4983=( BOUNDED_SURFACE ( )  B_SPLINE_SURFACE ( 3, 1, ( 
 ( #12266, #11032 ),
 ( #14606, #8621 ),
 ( #13519, #14683 ),
 ( #4086, #5313 ) ),
 .UNSPECIFIED., .F., .F., .T. ) 
 B_SPLINE_SURFACE_WITH_KNOTS ( ( 4, 4 ),
 ( 2, 2 ),
 ( 0.000000000000000000, 1.000000000000000000 ),
 ( 0.000000000000000000, 1.000000000000000000 ),
 .UNSPECIFIED. ) 
 GEOMETRIC_REPRESENTATION_ITEM ( )  RATIONAL_B_SPLINE_SURFACE ( (
 ( 1.000000000000000000, 1.000000000000000000),
 ( 0.9216682375510407699, 0.9216682375510407699),
 ( 0.9216682375510407699, 0.9216682375510407699),
 ( 1.000000000000000000, 1.000000000000000000) ) ) 
 REPRESENTATION_ITEM ( '' )  SURFACE ( )  );
#5013=DIRECTION ( 'NONE',  ( 0.000000000000000000, 0.000000000000000000, 1.000000000000000000 ) ) ;
#5042=CARTESIAN_POINT ( 'NONE',  ( -0.9087754948914893438, -1.020558061026470176, -45.55632290616385660 ) ) ;
#5052=DIRECTION ( 'NONE',  ( -0.3090169943749621062, 0.000000000000000000, -0.9510565162951489793 ) ) ;
#5064=ORIENTED_EDGE ( 'NONE', *, *, #9243, .F. ) ;
#5069=EDGE_LOOP ( 'NONE', ( #4546, #2666 ) ) ;
#5088=ADVANCED_FACE ( 'NONE', ( #6491 ), #14153, .F. ) ;
#5196=CARTESIAN_POINT ( 'NONE',  ( 7.995229681650333653, -1.921202954650397032, -34.56909192082981974 ) ) ;
#5211=CIRCLE ( 'NONE', #5693, 2.999999999999999112 ) ;
#5257=CARTESIAN_POINT ( 'NONE',  ( -3.306254070109473808, 2.579293035051157368, -1.000000000000001332 ) ) ;
#5286=CARTESIAN_POINT ( 'NONE',  ( 7.753811188820757039, 2.743867526398027223, -39.64929316069591891 ) ) ;
#5312=VERTEX_POINT ( 'NONE', #4028 ) ;
#5313=CARTESIAN_POINT ( 'NONE',  ( -4.878690035801932723, 0.000000000000000000, -0.3860167444088152822 ) ) ;
#5335=CARTESIAN_POINT ( 'NONE',  ( -8.842600465860288139, -2.075239479414269894, -40.10276331981361864 ) ) ;
#5347=EDGE_CURVE ( 'NONE', #6217, #1578, #28, .T. ) ;
#5367=ORIENTED_EDGE ( 'NONE', *, *, #9328, .F. ) ;
#5381=CARTESIAN_POINT ( 'NONE',  ( -8.671560925439079526, -2.743867526398025891, -35.09585054340071508 ) ) ;
#5406=LINE ( 'NONE', #10121, #9473 ) ;
#5426=CARTESIAN_POINT ( 'NONE',  ( 4.716951098700680411, 2.490287375297123962, -44.10818225254242009 ) ) ;
#5451=EDGE_CURVE ( 'NONE', #5655, #1404, #7585, .T. ) ;
#5456=AXIS2_PLACEMENT_3D ( 'NONE', #10847, #2427, #2510 ) ;
#5481=CARTESIAN_POINT ( 'NONE',  ( -3.055795963278728600, 2.474488745542203549, -1.000000000000011990 ) ) ;
#5504=CARTESIAN_POINT ( 'NONE',  ( -0.5793326530874193248, 2.075239479414269894, -43.47630266472464911 ) ) ;
#5518=ADVANCED_FACE ( 'NONE', ( #2904 ), #5692, .T. ) ;
#5531=CARTESIAN_POINT ( 'NONE',  ( -3.219147294323990938, -2.743867526398025891, -0.6706657213131048678 ) ) ;
#5562=FACE_OUTER_BOUND ( 'NONE', #3432, .T. ) ;
#5566=CARTESIAN_POINT ( 'NONE',  ( -0.4453226528549816265, -2.225540348348185052E-17, -1.000000000000000000 ) ) ;
#5614=SHAPE_DEFINITION_REPRESENTATION ( #10650, #4394 ) ;
#5638=CARTESIAN_POINT ( 'NONE',  ( 1.237310451418919932, -2.473751543678972542, -1.000000000000001332 ) ) ;
#5655=VERTEX_POINT ( 'NONE', #15044 ) ;
#5677=CARTESIAN_POINT ( 'NONE',  ( -8.289881740238502772, -2.529993217055221510, -35.21986562831451550 ) ) ;
#5692=TOROIDAL_SURFACE ( 'NONE', #9891, 4.000000000000000000, 1.000000000000000000 ) ;
#5693=AXIS2_PLACEMENT_3D ( 'NONE', #7790, #8797, #10032 ) ;
#5752=CARTESIAN_POINT ( 'NONE',  ( 1.831246893856133928, -2.490287375297125294, -1.000000000000000888 ) ) ;
#5774=CARTESIAN_POINT ( 'NONE',  ( -10.29275726619094478, 1.020558061026469510, -34.56909192082969895 ) ) ;
#5782=DIRECTION ( 'NONE',  ( 1.000000000000000000, 0.000000000000000000, -0.000000000000000000 ) ) ;
#5789=EDGE_CURVE ( 'NONE', #4779, #9239, #13726, .T. ) ;
#5807=ORIENTED_EDGE ( 'NONE', *, *, #9865, .T. ) ;
#5829=EDGE_CURVE ( 'NONE', #9311, #9630, #4099, .T. ) ;
#5831=ORIENTED_EDGE ( 'NONE', *, *, #11568, .T. ) ;
#5832=EDGE_CURVE ( 'NONE', #12909, #814, #2246, .T. ) ;
#5844=CARTESIAN_POINT ( 'NONE',  ( -9.836272398077417378, 1.921202954650395700, -34.71741284551207229 ) ) ;
#5909=CARTESIAN_POINT ( 'NONE',  ( 7.148068729939690336, -2.490287375297125294, -34.56909192082981974 ) ) ;
#5911=CARTESIAN_POINT ( 'NONE',  ( 2.920755695452265766, 1.195290186917868480, -1.000000000000001110 ) ) ;
#5915=CARTESIAN_POINT ( 'NONE',  ( -9.742503157198443731, 2.490287375297125294, -40.35209559314896666 ) ) ;
#5928=ORIENTED_EDGE ( 'NONE', *, *, #14445, .T. ) ;
#5946=CIRCLE ( 'NONE', #7933, 3.000000000000000000 ) ;
#5948=CARTESIAN_POINT ( 'NONE',  ( 7.148068729939690336, -2.490287375297125294, -34.56909192082981974 ) ) ;
#5975=ORIENTED_EDGE ( 'NONE', *, *, #13596, .F. ) ;
#6036=CARTESIAN_POINT ( 'NONE',  ( 8.475206276408092876, 0.000000000000000000, -34.56909192082981974 ) ) ;
#6039=CARTESIAN_POINT ( 'NONE',  ( -0.9087754948914270603, 0.000000000000000000, -36.05536862169275025 ) ) ;
#6103=CARTESIAN_POINT ( 'NONE',  ( -5.445322652854981627, 5.900679960901947346E-16, 1.000000000000000000 ) ) ;
#6176=CIRCLE ( 'NONE', #3463, 0.5000000000000017764 ) ;
#6195=CARTESIAN_POINT ( 'NONE',  ( -11.27598888897756346, 0.000000000000000000, -40.77697206847459910 ) ) ;
#6206=DIRECTION ( 'NONE',  ( 1.000000000000000000, 0.000000000000000000, 0.000000000000000000 ) ) ;
#6214=CARTESIAN_POINT ( 'NONE',  ( -8.289881740238502772, 2.075239479414269894, -35.21986562831451550 ) ) ;
#6217=VERTEX_POINT ( 'NONE', #11744 ) ;
#6246=FACE_OUTER_BOUND ( 'NONE', #12423, .T. ) ;
#6293=CARTESIAN_POINT ( 'NONE',  ( 4.554677347145018373, -2.225540348348185052E-17, 1.000000000000000000 ) ) ;
#6334=B_SPLINE_CURVE_WITH_KNOTS ( 'NONE', 3,
 ( #12614, #11598, #1018, #943, #12843, #13780, #720, #3179, #7890, #873 ),
 .UNSPECIFIED., .F., .F.,
 ( 4, 2, 2, 2, 4 ),
 ( 0.000000000000000000, 0.0002702708960404994203, 0.0005405417920809988406, 0.0008108126881214983150, 0.001081083584161997681 ),
 .UNSPECIFIED. ) ;
#6342=CARTESIAN_POINT ( 'NONE',  ( 4.329912723285513465, -2.529993217055220178, -43.25836301743402856 ) ) ;
#6363=CARTESIAN_POINT ( 'NONE',  ( -8.289881740238515206, 2.075239479414269894, -35.21986562831452261 ) ) ;
#6436=CARTESIAN_POINT ( 'NONE',  ( -8.842600465860288139, 2.529993217055222399, -40.10276331981361153 ) ) ;
#6438=DIRECTION ( 'NONE',  ( 0.1564344650402314796, 0.000000000000000000, 0.9876883405951375483 ) ) ;
#6449=CIRCLE ( 'NONE', #2256, 5.000000000000000000 ) ;
#6476=EDGE_CURVE ( 'NONE', #5312, #10124, #10203, .T. ) ;
#6491=FACE_OUTER_BOUND ( 'NONE', #2013, .T. ) ;
#6497=CARTESIAN_POINT ( 'NONE',  ( 6.770579566034210295, -2.743867526398025447, -34.56909192082981974 ) ) ;
#6499=EDGE_CURVE ( 'NONE', #505, #4779, #5406, .T. ) ;
#6505=CARTESIAN_POINT ( 'NONE',  ( 8.475206276408092876, -1.020558061026469288, -34.56909192082981974 ) ) ;
#6551=CARTESIAN_POINT ( 'NONE',  ( -4.946131244327882648, 0.4878928319774004096, -1.000000000000001554 ) ) ;
#6563=ADVANCED_FACE ( 'NONE', ( #2231 ), #1147, .T. ) ;
#6592=CARTESIAN_POINT ( 'NONE',  ( -9.306320601523868419, 2.743867526398027223, -40.23124431751398333 ) ) ;
#6593=CIRCLE ( 'NONE', #8553, 0.5000000000000004441 ) ;
#6617=CARTESIAN_POINT ( 'NONE',  ( 3.158384440324536691, 0.000000000000000000, -1.000000000000001332 ) ) ;
#6662=DIRECTION ( 'NONE',  ( -0.9510565162951478690, 0.000000000000000000, 0.3090169943749654369 ) ) ;
#6664=CARTESIAN_POINT ( 'NONE',  ( -8.671560925439095513, 2.743867526398027223, -35.09585054340072219 ) ) ;
#6689=LINE ( 'NONE', #10311, #13589 ) ;
#6707=CARTESIAN_POINT ( 'NONE',  ( -4.975935430107378821, 0.000000000000000000, -1.000000000000001332 ) ) ;
#6721=CARTESIAN_POINT ( 'NONE',  ( 4.529353718053118705, -2.743867526398026335, -43.69627513258503626 ) ) ;
#6757=CARTESIAN_POINT ( 'NONE',  ( -3.213772066606566558, -2.558678233169556115, -1.000000000000011990 ) ) ;
#6783=ADVANCED_FACE ( 'NONE', ( #903 ), #12657, .F. ) ;
#6882=DIRECTION ( 'NONE',  ( 0.9876883405951377704, 0.000000000000000000, 0.1564344650402315628 ) ) ;
#6969=ORIENTED_EDGE ( 'NONE', *, *, #8776, .F. ) ;
#6990=ORIENTED_EDGE ( 'NONE', *, *, #647, .F. ) ;
#7048=DIRECTION ( 'NONE',  ( 1.000000000000000000, 0.000000000000000000, 0.000000000000000000 ) ) ;
#7072=CARTESIAN_POINT ( 'NONE',  ( 5.376486659670671742, 1.020558061026469510, -45.55632290616389923 ) ) ;
#7144=CARTESIAN_POINT ( 'NONE',  ( 9.458437899194636955, 1.020558061026469510, -40.77697206847473410 ) ) ;
#7149=DIRECTION ( 'NONE',  ( 0.000000000000000000, 0.000000000000000000, 1.000000000000000000 ) ) ;
#7188=FACE_OUTER_BOUND ( 'NONE', #10528, .T. ) ;
#7213=EDGE_LOOP ( 'NONE', ( #11808, #11111, #14578, #9378 ) ) ;
#7221=ADVANCED_BREP_SHAPE_REPRESENTATION ( '', ( #2311, #9419 ), #14368 ) ;
#7230=AXIS2_PLACEMENT_3D ( 'NONE', #11431, #7948, #5782 ) ;
#7244=ORIENTED_EDGE ( 'NONE', *, *, #13596, .T. ) ;
#7272=CARTESIAN_POINT ( 'NONE',  ( 8.131300352726233527, -2.490287375297126626, -39.89901737624450107 ) ) ;
#7308=CARTESIAN_POINT ( 'NONE',  ( 3.554677347145018373, -2.225540348348185052E-17, 2.000000000000000000 ) ) ;
#7383=DIRECTION ( 'NONE',  ( 0.000000000000000000, 1.000000000000000000, 0.000000000000000000 ) ) ;
#7424=ORIENTED_EDGE ( 'NONE', *, *, #8346, .F. ) ;
#7433=AXIS2_PLACEMENT_3D ( 'NONE', #9412, #7149, #14137 ) ;
#7470=CARTESIAN_POINT ( 'NONE',  ( -10.29275726619092524, 1.020558061026469066, -34.56909192082969184 ) ) ;
#7535=CARTESIAN_POINT ( 'NONE',  ( -3.648797883638980277, -2.490287375297125294, -1.000000000000000888 ) ) ;
#7559=CARTESIAN_POINT ( 'NONE',  ( -0.9087754948914270603, 2.490287375297123962, -36.05536862169275025 ) ) ;
#7567=DIRECTION ( 'NONE',  ( 0.000000000000000000, 1.000000000000000000, 0.000000000000000000 ) ) ;
#7585=B_SPLINE_CURVE_WITH_KNOTS ( 'NONE', 3,
 ( #3084, #11347, #2003, #7798, #5481, #10199, #5257, #14707, #4107, #2937 ),
 .UNSPECIFIED., .F., .F.,
 ( 4, 2, 2, 2, 4 ),
 ( 0.000000000000000000, 0.0002702708960404937824, 0.0005405417920809875649, 0.0008108126881214814015, 0.001081083584161975130 ),
 .UNSPECIFIED. ) ;
#7589=ADVANCED_FACE ( 'NONE', ( #11065 ), #13056, .F. ) ;
#7598=CARTESIAN_POINT ( 'NONE',  ( 1.052436484934202499, -2.075239479414269894, -1.000000000000000888 ) ) ;
#7604=ORIENTED_EDGE ( 'NONE', *, *, #2525, .F. ) ;
#7617=ORIENTED_EDGE ( 'NONE', *, *, #14636, .F. ) ;
#7660=CIRCLE ( 'NONE', #11, 9.500954284471095690 ) ;
#7666=AXIS2_PLACEMENT_3D ( 'NONE', #2586, #12310, #2894 ) ;
#7678=ADVANCED_FACE ( 'NONE', ( #8971 ), #10404, .T. ) ;
#7699=ADVANCED_FACE ( 'NONE', ( #11142 ), #11897, .T. ) ;
#7711=CARTESIAN_POINT ( 'NONE',  ( -0.9087754948914270603, -2.075239479414269894, -36.05536862169275025 ) ) ;
#7741=CIRCLE ( 'NONE', #7981, 4.000000000000000000 ) ;
#7790=CARTESIAN_POINT ( 'NONE',  ( -7.439587717305479408, 0.000000000000000000, -35.49614290395457772 ) ) ;
#7798=CARTESIAN_POINT ( 'NONE',  ( -2.987892022880174636, 2.410101856083632477, -1.000000000000001110 ) ) ;
#7803=CARTESIAN_POINT ( 'NONE',  ( -8.842600465860286363, -2.529993217055220178, -40.10276331981361864 ) ) ;
#7877=EDGE_LOOP ( 'NONE', ( #10173, #4085, #2087, #3890, #8162 ) ) ;
#7890=CARTESIAN_POINT ( 'NONE',  ( 1.756204145886661516, 2.540697700117988678, -1.000000000000001110 ) ) ;
#7910=( BOUNDED_SURFACE ( )  B_SPLINE_SURFACE ( 3, 1, ( 
 ( #9844, #14577 ),
 ( #3312, #9411 ),
 ( #4473, #4397 ),
 ( #3231, #9183 ) ),
 .UNSPECIFIED., .F., .F., .F. ) 
 B_SPLINE_SURFACE_WITH_KNOTS ( ( 4, 4 ),
 ( 2, 2 ),
 ( 0.000000000000000000, 1.000000000000000000 ),
 ( 0.000000000000000000, 1.000000000000000000 ),
 .UNSPECIFIED. ) 
 GEOMETRIC_REPRESENTATION_ITEM ( )  RATIONAL_B_SPLINE_SURFACE ( (
 ( 1.000000000000000000, 1.000000000000000000),
 ( 0.6468719831415912225, 0.6468719831415912225),
 ( 0.6468719831415912225, 0.6468719831415912225),
 ( 1.000000000000000000, 1.000000000000000000) ) ) 
 REPRESENTATION_ITEM ( '' )  SURFACE ( )  );
#7911=CARTESIAN_POINT ( 'NONE',  ( -3.648797883638980277, -2.490287375297125294, -1.000000000000000888 ) ) ;
#7925=CIRCLE ( 'NONE', #5456, 0.5000000000000001110 ) ;
#7927=CARTESIAN_POINT ( 'NONE',  ( -8.289881740238502772, -2.075239479414269894, -35.21986562831451550 ) ) ;
#7933=AXIS2_PLACEMENT_3D ( 'NONE', #14232, #12994, #3403 ) ;
#7948=DIRECTION ( 'NONE',  ( 0.000000000000000000, 0.000000000000000000, 1.000000000000000000 ) ) ;
#7981=AXIS2_PLACEMENT_3D ( 'NONE', #9527, #13321, #3889 ) ;
#7996=ORIENTED_EDGE ( 'NONE', *, *, #1604, .T. ) ;
#8029=ORIENTED_EDGE ( 'NONE', *, *, #3454, .T. ) ;
#8057=ADVANCED_FACE ( 'NONE', ( #11362 ), #934, .T. ) ;
#8061=CARTESIAN_POINT ( 'NONE',  ( -0.4453226528549816265, -2.225540348348185052E-17, 1.000000000000000000 ) ) ;
#8138=EDGE_CURVE ( 'NONE', #2052, #9239, #13652, .T. ) ;
#8160=CARTESIAN_POINT ( 'NONE',  ( 2.220649286760296270, 2.192442743657398108, -1.000000000000001776 ) ) ;
#8162=ORIENTED_EDGE ( 'NONE', *, *, #14507, .T. ) ;
#8170=CARTESIAN_POINT ( 'NONE',  ( -3.852746828226704334, -2.353283696435566785, -1.000000000000007772 ) ) ;
#8173=APPLICATION_CONTEXT ( 'configuration controlled 3d designs of mechanical parts and assemblies' ) ;
#8222=ORIENTED_EDGE ( 'NONE', *, *, #12623, .T. ) ;
#8235=CARTESIAN_POINT ( 'NONE',  ( -8.671560925439088408, -2.743867526398025447, -35.09585054340072219 ) ) ;
#8241=CARTESIAN_POINT ( 'NONE',  ( -7.194037649453649763, 1.020558061026469510, -45.55632290616381397 ) ) ;
#8253=EDGE_LOOP ( 'NONE', ( #12826, #10823, #8222, #6990 ) ) ;
#8297=VERTEX_POINT ( 'NONE', #4102 ) ;
#8301=ORIENTED_EDGE ( 'NONE', *, *, #5832, .T. ) ;
#8309=CARTESIAN_POINT ( 'NONE',  ( 3.009961423602985242, 0.9636447990543508535, -1.000000000000001332 ) ) ;
#8313=CARTESIAN_POINT ( 'NONE',  ( 8.475206276408092876, 0.000000000000000000, -34.56909192082981974 ) ) ;
#8346=EDGE_CURVE ( 'NONE', #8297, #10459, #1770, .T. ) ;
#8356=DIRECTION ( 'NONE',  ( 0.000000000000000000, 0.000000000000000000, 1.000000000000000000 ) ) ;
#8357=( LENGTH_UNIT ( ) NAMED_UNIT ( * ) SI_UNIT ( .MILLI., .METRE. ) );
#8384=CARTESIAN_POINT ( 'NONE',  ( 3.128580254545037853, 0.4878928319773999656, -1.000000000000001110 ) ) ;
#8389=CARTESIAN_POINT ( 'NONE',  ( -0.7011654427748897911, 2.490287375297125294, -44.24552462515097062 ) ) ;
#8411=CARTESIAN_POINT ( 'NONE',  ( 1.831246893856133928, -2.490287375297125294, -1.000000000000000888 ) ) ;
#8427=ORIENTED_EDGE ( 'NONE', *, *, #6499, .T. ) ;
#8443=PRODUCT_DEFINITION_FORMATION_WITH_SPECIFIED_SOURCE ( 'ANY', '', #14121, .NOT_KNOWN. ) ;
#8457=CARTESIAN_POINT ( 'NONE',  ( -2.869987474717050624, -2.075239479414269894, -1.000000000000000888 ) ) ;
#8469=CARTESIAN_POINT ( 'NONE',  ( 5.376486659670670853, 0.000000000000000000, -45.55632290616389923 ) ) ;
#8509=CARTESIAN_POINT ( 'NONE',  ( -6.805338252203101845, -1.921202954650397476, -45.13192727926511338 ) ) ;
#8516=B_SPLINE_CURVE_WITH_KNOTS ( 'NONE', 3,
 ( #3073, #10329, #12500, #11337, #761, #1845, #15068, #6551, #1917, #6707 ),
 .UNSPECIFIED., .F., .F.,
 ( 4, 2, 2, 2, 4 ),
 ( 9.697399036122160616E-19, 0.0007311508082448070923, 0.001462301616489613100, 0.002193452424734419325, 0.002924603232979225333 ),
 .UNSPECIFIED. ) ;
#8527=ORIENTED_EDGE ( 'NONE', *, *, #4420, .F. ) ;
#8533=ORIENTED_EDGE ( 'NONE', *, *, #13980, .F. ) ;
#8553=AXIS2_PLACEMENT_3D ( 'NONE', #9582, #13309, #9823 ) ;
#8581=VERTEX_POINT ( 'NONE', #7308 ) ;
#8585=CARTESIAN_POINT ( 'NONE',  ( -11.27598888897756702, -1.020558061026470176, -40.77697206847461331 ) ) ;
#8595=( NAMED_UNIT ( * ) PLANE_ANGLE_UNIT ( ) SI_UNIT ( $, .RADIAN. ) );
#8621=CARTESIAN_POINT ( 'NONE',  ( -4.422205167688408878, -1.921202954650395478, -0.5343376690911894045 ) ) ;
#8632=CARTESIAN_POINT ( 'NONE',  ( -8.289881740238500996, 2.529993217055223287, -35.21986562831451550 ) ) ;
#8644=DIRECTION ( 'NONE',  ( 0.000000000000000000, 0.000000000000000000, 1.000000000000000000 ) ) ;
#8654=CARTESIAN_POINT ( 'NONE',  ( -8.289881740238515206, -2.075239479414269894, -35.21986562831452261 ) ) ;
#8655=ADVANCED_FACE ( 'NONE', ( #10638 ), #13977, .F. ) ;
#8720=DIRECTION ( 'NONE',  ( 0.000000000000000000, 0.000000000000000000, 1.000000000000000000 ) ) ;
#8727=CARTESIAN_POINT ( 'NONE',  ( -2.869987474717051068, -2.075239479414269894, -1.000000000000004441 ) ) ;
#8732=DIRECTION ( 'NONE',  ( 0.000000000000000000, 0.000000000000000000, 1.000000000000000000 ) ) ;
#8741=DIRECTION ( 'NONE',  ( 0.1564344650402314796, 0.000000000000000000, 0.9876883405951375483 ) ) ;
#8755=ADVANCED_FACE ( 'NONE', ( #2302 ), #2320, .F. ) ;
#8758=CARTESIAN_POINT ( 'NONE',  ( 8.475206276408092876, 1.020558061026468177, -34.56909192082981974 ) ) ;
#8762=CARTESIAN_POINT ( 'NONE',  ( 7.352489943804304318, 2.529993217055222399, -39.38380306805898101 ) ) ;
#8776=EDGE_CURVE ( 'NONE', #505, #12985, #14665, .T. ) ;
#8785=ORIENTED_EDGE ( 'NONE', *, *, #4780, .F. ) ;
#8796=CARTESIAN_POINT ( 'NONE',  ( -2.837468109123920890, 2.075239479414269894, -0.7946808062301163877 ) ) ;
#8797=DIRECTION ( 'NONE',  ( -0.3090169943749621062, 0.000000000000000000, -0.9510565162951489793 ) ) ;
#8817=DESIGN_CONTEXT ( 'detailed design', #8173, 'design' ) ;
#8823=DIRECTION ( 'NONE',  ( 1.000000000000000000, 0.000000000000000000, 0.000000000000000000 ) ) ;
#8833=ADVANCED_FACE ( 'NONE', ( #9946 ), #4983, .F. ) ;
#8876=DIRECTION ( 'NONE',  ( -0.1564344650402312298, -0.000000000000000000, 0.9876883405951376593 ) ) ;
#8897=DIRECTION ( 'NONE',  ( 0.000000000000000000, 0.000000000000000000, 1.000000000000000000 ) ) ;
#8937=ORIENTED_EDGE ( 'NONE', *, *, #1292, .F. ) ;
#8971=FACE_OUTER_BOUND ( 'NONE', #8253, .T. ) ;
#8982=DIRECTION ( 'NONE',  ( 0.000000000000000000, 1.000000000000000000, 0.000000000000000000 ) ) ;
#8984=CARTESIAN_POINT ( 'NONE',  ( 6.369258321017759350, 2.075239479414269894, -34.56909192082981974 ) ) ;
#9051=CARTESIAN_POINT ( 'NONE',  ( 2.678407845566781020, -1.921202954650395700, -1.000000000000023537 ) ) ;
#9061=CARTESIAN_POINT ( 'NONE',  ( -0.6421131273608506884, 2.743867526398027223, -43.87268297926053151 ) ) ;
#9085=ORIENTED_EDGE ( 'NONE', *, *, #219, .F. ) ;
#9111=EDGE_LOOP ( 'NONE', ( #3574, #4901, #7604, #2323 ) ) ;
#9113=CARTESIAN_POINT ( 'NONE',  ( 7.148068729939690336, -2.490287375297125294, -34.56909192082981974 ) ) ;
#9140=VERTEX_POINT ( 'NONE', #9618 ) ;
#9183=CARTESIAN_POINT ( 'NONE',  ( 1.052436484934206939, 2.075239479414269894, -1.000000000000028644 ) ) ;
#9198=CARTESIAN_POINT ( 'NONE',  ( 1.756204145889998625, -2.540697700116526736, -1.000000000000007772 ) ) ;
#9226=DIRECTION ( 'NONE',  ( 0.000000000000000000, 0.000000000000000000, 1.000000000000000000 ) ) ;
#9237=ORIENTED_EDGE ( 'NONE', *, *, #13666, .F. ) ;
#9239=VERTEX_POINT ( 'NONE', #10855 ) ;
#9243=EDGE_CURVE ( 'NONE', #9630, #5655, #9783, .T. ) ;
#9300=VECTOR ( 'NONE', #3875, 1000.000000000000114 ) ;
#9301=CARTESIAN_POINT ( 'NONE',  ( 5.475206276408092876, 0.000000000000000000, -34.56909192082981974 ) ) ;
#9311=VERTEX_POINT ( 'NONE', #7535 ) ;
#9328=EDGE_CURVE ( 'NONE', #3650, #814, #12763, .T. ) ;
#9348=CARTESIAN_POINT ( 'NONE',  ( 1.052436484934852201, -2.165641995260652486, -1.000000000000001110 ) ) ;
#9378=ORIENTED_EDGE ( 'NONE', *, *, #14507, .F. ) ;
#9395=VECTOR ( 'NONE', #5013, 1000.000000000000000 ) ;
#9399=CARTESIAN_POINT ( 'NONE',  ( -0.6421131273608509105, -2.743867526398025447, -43.87268297926051730 ) ) ;
#9404=( BOUNDED_SURFACE ( )  B_SPLINE_SURFACE ( 3, 1, ( 
 ( #9839, #9920 ),
 ( #8758, #649 ),
 ( #10069, #1717 ),
 ( #13329, #14804 ) ),
 .UNSPECIFIED., .F., .F., .F. ) 
 B_SPLINE_SURFACE_WITH_KNOTS ( ( 4, 4 ),
 ( 2, 2 ),
 ( 0.000000000000000000, 1.000000000000000000 ),
 ( 0.000000000000000000, 1.000000000000000000 ),
 .UNSPECIFIED. ) 
 GEOMETRIC_REPRESENTATION_ITEM ( )  RATIONAL_B_SPLINE_SURFACE ( (
 ( 1.000000000000000000, 1.000000000000000000),
 ( 0.9216682375510409919, 0.9216682375510409919),
 ( 0.9216682375510409919, 0.9216682375510409919),
 ( 1.000000000000000000, 1.000000000000000000) ) ) 
 REPRESENTATION_ITEM ( '' )  SURFACE ( )  );
#9408=CARTESIAN_POINT ( 'NONE',  ( 4.716951098700676859, 2.490287375297125294, -44.10818225254241298 ) ) ;
#9411=CARTESIAN_POINT ( 'NONE',  ( 1.453757729950659217, 2.743867526398027223, -1.000000000000029088 ) ) ;
#9412=CARTESIAN_POINT ( 'NONE',  ( 6.869258321017759350, -2.075239479414269894, -34.56909192082981974 ) ) ;
#9419=AXIS2_PLACEMENT_3D ( 'NONE', #15272, #9226, #12943 ) ;
#9463=CARTESIAN_POINT ( 'NONE',  ( 2.219068112418553174, -2.193945312325717101, -1.000000000000001110 ) ) ;
#9473=VECTOR ( 'NONE', #12515, 1000.000000000000000 ) ;
#9482=CARTESIAN_POINT ( 'NONE',  ( -4.878690035801932723, 0.000000000000000000, -0.3860167444088152822 ) ) ;
#9486=CARTESIAN_POINT ( 'NONE',  ( -4.975935430107380597, -0.4889170748306866376, -1.000000000000011990 ) ) ;
#9501=ORIENTED_EDGE ( 'NONE', *, *, #219, .T. ) ;
#9513=ADVANCED_FACE ( 'NONE', ( #2785 ), #12432, .T. ) ;
#9527=CARTESIAN_POINT ( 'NONE',  ( -0.4453226528549816265, -2.225540348348185052E-17, 2.000000000000000000 ) ) ;
#9554=CARTESIAN_POINT ( 'NONE',  ( -0.9087754948914893438, 1.020558061026469510, -45.55632290616385660 ) ) ;
#9582=CARTESIAN_POINT ( 'NONE',  ( 6.869258321017759350, 2.075239479414269450, -34.56909192082981974 ) ) ;
#9595=DIRECTION ( 'NONE',  ( 0.000000000000000000, 0.000000000000000000, 1.000000000000000000 ) ) ;
#9596=ORIENTED_EDGE ( 'NONE', *, *, #13782, .T. ) ;
#9603=( NAMED_UNIT ( * ) SI_UNIT ( $, .STERADIAN. ) SOLID_ANGLE_UNIT ( ) );
#9618=CARTESIAN_POINT ( 'NONE',  ( -4.445322652854981627, 5.288356561328269633E-16, 2.000000000000000000 ) ) ;
#9630=VERTEX_POINT ( 'NONE', #8727 ) ;
#9645=DIRECTION ( 'NONE',  ( -0.000000000000000000, -0.000000000000000000, -1.000000000000000000 ) ) ;
#9767=LINE ( 'NONE', #1803, #14592 ) ;
#9783=LINE ( 'NONE', #8457, #2314 ) ;
#9823=DIRECTION ( 'NONE',  ( 1.000000000000000000, 0.000000000000000000, 0.000000000000000000 ) ) ;
#9831=CARTESIAN_POINT ( 'NONE',  ( 4.716951098700676859, -2.490287375297126626, -44.10818225254241298 ) ) ;
#9839=CARTESIAN_POINT ( 'NONE',  ( 8.475206276408092876, 0.000000000000000000, -34.56909192082981974 ) ) ;
#9844=CARTESIAN_POINT ( 'NONE',  ( 7.148068729939693000, 2.490287375297123962, -34.56909192082981974 ) ) ;
#9865=EDGE_CURVE ( 'NONE', #13794, #1404, #10994, .T. ) ;
#9877=CARTESIAN_POINT ( 'NONE',  ( -2.837468109123920446, 2.529993217055223287, -0.7946808062301191633 ) ) ;
#9891=AXIS2_PLACEMENT_3D ( 'NONE', #4843, #13432, #3611 ) ;
#9897=CARTESIAN_POINT ( 'NONE',  ( -0.5793326530874193248, -2.529993217055220178, -43.47630266472464911 ) ) ;
#9899=CIRCLE ( 'NONE', #15105, 5.000000000000000000 ) ;
#9910=CARTESIAN_POINT ( 'NONE',  ( 8.978461304436876844, -1.921202954650397476, -40.45944830867332342 ) ) ;
#9920=CARTESIAN_POINT ( 'NONE',  ( 3.158384440324541131, 0.000000000000000000, -1.000000000000028644 ) ) ;
#9939=CARTESIAN_POINT ( 'NONE',  ( -0.4453226528549816265, -2.225540348348185052E-17, -1.000000000000000000 ) ) ;
#9946=FACE_OUTER_BOUND ( 'NONE', #7213, .T. ) ;
#9982=CARTESIAN_POINT ( 'NONE',  ( 3.158384440324538467, -1.020558061026469288, -1.000000000000023537 ) ) ;
#9993=EDGE_CURVE ( 'NONE', #9140, #8581, #7741, .T. ) ;
#9998=CARTESIAN_POINT ( 'NONE',  ( 7.352489943804302541, 2.075239479414269894, -39.38380306805896680 ) ) ;
#10032=DIRECTION ( 'NONE',  ( -0.9510565162951488682, 0.000000000000000000, 0.3090169943749619952 ) ) ;
#10056=EDGE_CURVE ( 'NONE', #814, #9140, #3299, .T. ) ;
#10069=CARTESIAN_POINT ( 'NONE',  ( 7.995229681650334541, 1.921202954650393924, -34.56909192082981974 ) ) ;
#10077=ADVANCED_FACE ( 'NONE', ( #7188 ), #11911, .F. ) ;
#10093=ORIENTED_EDGE ( 'NONE', *, *, #708, .T. ) ;
#10121=CARTESIAN_POINT ( 'NONE',  ( 6.369258321017759350, -2.075239479414269894, -34.56909192082981974 ) ) ;
#10124=VERTEX_POINT ( 'NONE', #3966 ) ;
#10126=CARTESIAN_POINT ( 'NONE',  ( 1.052436484934206051, -2.075239479414269894, -1.000000000000021760 ) ) ;
#10148=CARTESIAN_POINT ( 'NONE',  ( -5.813579972774825855, 2.743867526398027223, -44.04909082593602676 ) ) ;
#10149=PLANE ( 'NONE',  #2338 ) ;
#10170=B_SPLINE_CURVE_WITH_KNOTS ( 'NONE', 3,
 ( #6617, #11325, #11703, #4670, #10474, #9463, #1121, #5752 ),
 .UNSPECIFIED., .F., .F.,
 ( 4, 2, 2, 4 ),
 ( 0.002924603232979224900, 0.004377839289350649032, 0.005104457317536361532, 0.005831075345722074033 ),
 .UNSPECIFIED. ) ;
#10173=ORIENTED_EDGE ( 'NONE', *, *, #5829, .T. ) ;
#10177=ORIENTED_EDGE ( 'NONE', *, *, #4765, .T. ) ;
#10191=ORIENTED_EDGE ( 'NONE', *, *, #708, .F. ) ;
#10199=CARTESIAN_POINT ( 'NONE',  ( -3.214905123735726900, 2.559042896907052889, -1.000000000000011768 ) ) ;
#10203=LINE ( 'NONE', #701, #1581 ) ;
#10280=EDGE_LOOP ( 'NONE', ( #5064, #15016, #10965, #12318 ) ) ;
#10311=CARTESIAN_POINT ( 'NONE',  ( 6.369258321017759350, 2.075239479414269894, -34.56909192082981974 ) ) ;
#10329=CARTESIAN_POINT ( 'NONE',  ( -3.854019100140201104, 2.352429041693352652, -1.000000000000004441 ) ) ;
#10404=( BOUNDED_SURFACE ( )  B_SPLINE_SURFACE ( 3, 1, ( 
 ( #11364, #639 ),
 ( #12603, #9051 ),
 ( #6505, #9982 ),
 ( #4121, #790 ) ),
 .UNSPECIFIED., .F., .F., .F. ) 
 B_SPLINE_SURFACE_WITH_KNOTS ( ( 4, 4 ),
 ( 2, 2 ),
 ( 0.000000000000000000, 1.000000000000000000 ),
 ( 0.000000000000000000, 1.000000000000000000 ),
 .UNSPECIFIED. ) 
 GEOMETRIC_REPRESENTATION_ITEM ( )  RATIONAL_B_SPLINE_SURFACE ( (
 ( 1.000000000000000000, 1.000000000000000000),
 ( 0.9216682375510407699, 0.9216682375510407699),
 ( 0.9216682375510407699, 0.9216682375510407699),
 ( 1.000000000000000000, 1.000000000000000000) ) ) 
 REPRESENTATION_ITEM ( '' )  SURFACE ( )  );
#10407=ORIENTED_EDGE ( 'NONE', *, *, #647, .T. ) ;
#10412=FACE_OUTER_BOUND ( 'NONE', #10477, .T. ) ;
#10436=CARTESIAN_POINT ( 'NONE',  ( 1.831246893856137481, 2.490287375297123074, -1.000000000000007772 ) ) ;
#10446=CARTESIAN_POINT ( 'NONE',  ( 6.369258321017759350, 2.075239479414269894, -34.56909192082981974 ) ) ;
#10459=VERTEX_POINT ( 'NONE', #10436 ) ;
#10470=AXIS2_PLACEMENT_3D ( 'NONE', #13701, #8897, #8823 ) ;
#10474=CARTESIAN_POINT ( 'NONE',  ( 2.547208780220832747, -1.831210392890420424, -1.000000000000001332 ) ) ;
#10477=EDGE_LOOP ( 'NONE', ( #4336, #2113 ) ) ;
#10494=( BOUNDED_SURFACE ( )  B_SPLINE_SURFACE ( 3, 1, ( 
 ( #12596, #10126 ),
 ( #3241, #860 ),
 ( #6497, #4404 ),
 ( #9113, #15088 ) ),
 .UNSPECIFIED., .F., .F., .T. ) 
 B_SPLINE_SURFACE_WITH_KNOTS ( ( 4, 4 ),
 ( 2, 2 ),
 ( 0.000000000000000000, 1.000000000000000000 ),
 ( 0.000000000000000000, 1.000000000000000000 ),
 .UNSPECIFIED. ) 
 GEOMETRIC_REPRESENTATION_ITEM ( )  RATIONAL_B_SPLINE_SURFACE ( (
 ( 1.000000000000000000, 1.000000000000000000),
 ( 0.6468719831415924437, 0.6468719831415924437),
 ( 0.6468719831415924437, 0.6468719831415924437),
 ( 1.000000000000000000, 1.000000000000000000) ) ) 
 REPRESENTATION_ITEM ( '' )  SURFACE ( )  );
#10512=CARTESIAN_POINT ( 'NONE',  ( 1.077013294873430338, -2.254417391461207565, -1.000000000000001110 ) ) ;
#10528=EDGE_LOOP ( 'NONE', ( #11513, #11702, #1272, #5975 ) ) ;
#10547=ORIENTED_EDGE ( 'NONE', *, *, #1292, .T. ) ;
#10604=DIRECTION ( 'NONE',  ( -0.000000000000000000, -0.000000000000000000, -1.000000000000000000 ) ) ;
#10630=CARTESIAN_POINT ( 'NONE',  ( -5.488578029460351893, -2.529993217055220178, -43.69424231201529096 ) ) ;
#10638=FACE_OUTER_BOUND ( 'NONE', #14035, .T. ) ;
#10639=VECTOR ( 'NONE', #14823, 1000.000000000000227 ) ;
#10650=PRODUCT_DEFINITION_SHAPE ( 'NONE', 'NONE',  #2984 ) ;
#10663=DIRECTION ( 'NONE',  ( 0.000000000000000000, -1.000000000000000000, 0.000000000000000000 ) ) ;
#10765=SHAPE_REPRESENTATION_RELATIONSHIP ( 'NONE' , 'NONE' ,  #4394, #7221 ) ;
#10819=LINE ( 'NONE', #4036, #14352 ) ;
#10823=ORIENTED_EDGE ( 'NONE', *, *, #6476, .T. ) ;
#10827=CARTESIAN_POINT ( 'NONE',  ( -7.194037649453649763, -1.020558061026470176, -45.55632290616381397 ) ) ;
#10847=CARTESIAN_POINT ( 'NONE',  ( -8.765409998386077817, -2.075239479414269894, -35.06535713112702979 ) ) ;
#10855=CARTESIAN_POINT ( 'NONE',  ( 1.052436484934202499, -2.075239479414269894, -1.000000000000000888 ) ) ;
#10921=DIRECTION ( 'NONE',  ( 0.1564344650402314796, 0.000000000000000000, 0.9876883405951375483 ) ) ;
#10928=ORIENTED_EDGE ( 'NONE', *, *, #12623, .F. ) ;
#10965=ORIENTED_EDGE ( 'NONE', *, *, #2054, .F. ) ;
#10991=CARTESIAN_POINT ( 'NONE',  ( 5.376486659670671742, -1.020558061026470176, -45.55632290616389923 ) ) ;
#10994=LINE ( 'NONE', #13165, #14425 ) ;
#11011=FACE_OUTER_BOUND ( 'NONE', #14992, .T. ) ;
#11028=ORIENTED_EDGE ( 'NONE', *, *, #8138, .F. ) ;
#11032=CARTESIAN_POINT ( 'NONE',  ( -3.616507224213203475, -2.490287375297124850, -0.7961248001406434627 ) ) ;
#11065=FACE_OUTER_BOUND ( 'NONE', #11484, .T. ) ;
#11075=CARTESIAN_POINT ( 'NONE',  ( 7.148068729939693000, 2.490287375297123962, -34.56909192082981974 ) ) ;
#11101=CARTESIAN_POINT ( 'NONE',  ( -9.836272398077403167, 1.921202954650395256, -34.71741284551207229 ) ) ;
#11111=ORIENTED_EDGE ( 'NONE', *, *, #1604, .F. ) ;
#11142=FACE_OUTER_BOUND ( 'NONE', #15070, .T. ) ;
#11157=CARTESIAN_POINT ( 'NONE',  ( -10.29275726619092524, 0.000000000000000000, -34.56909192082969184 ) ) ;
#11186=ADVANCED_FACE ( 'NONE', ( #6246 ), #232, .F. ) ;
#11199=DIRECTION ( 'NONE',  ( 1.000000000000000000, 0.000000000000000000, 0.000000000000000000 ) ) ;
#11209=CARTESIAN_POINT ( 'NONE',  ( 6.369258321017760238, -2.075239479414269894, -34.56909192082981974 ) ) ;
#11277=CARTESIAN_POINT ( 'NONE',  ( -0.9087754948914270603, -2.490287375297125294, -36.05536862169275025 ) ) ;
#11293=EDGE_CURVE ( 'NONE', #1404, #14984, #8516, .T. ) ;
#11305=DIRECTION ( 'NONE',  ( -0.9876883405951377704, 0.000000000000000000, -0.1564344650402312575 ) ) ;
#11325=CARTESIAN_POINT ( 'NONE',  ( 3.158384440324536246, -0.4889170748306868597, -1.000000000000001554 ) ) ;
#11326=ORIENTED_EDGE ( 'NONE', *, *, #1384, .T. ) ;
#11337=CARTESIAN_POINT ( 'NONE',  ( -4.365898909102353009, 1.829703814864835687, -1.000000000000011546 ) ) ;
#11347=CARTESIAN_POINT ( 'NONE',  ( -2.869987474717049292, 2.165641995257062025, -1.000000000000004663 ) ) ;
#11349=DIRECTION ( 'NONE',  ( 1.000000000000000000, 0.000000000000000000, 0.000000000000000000 ) ) ;
#11362=FACE_OUTER_BOUND ( 'NONE', #15133, .T. ) ;
#11364=CARTESIAN_POINT ( 'NONE',  ( 7.148068729939690336, -2.490287375297125294, -34.56909192082981974 ) ) ;
#11375=CIRCLE ( 'NONE', #7666, 4.000000000000000000 ) ;
#11380=CARTESIAN_POINT ( 'NONE',  ( -8.842600465860288139, 2.075239479414269894, -40.10276331981361864 ) ) ;
#11410=EDGE_LOOP ( 'NONE', ( #3691, #13429, #14343, #5831 ) ) ;
#11421=ORIENTED_EDGE ( 'NONE', *, *, #12628, .T. ) ;
#11431=CARTESIAN_POINT ( 'NONE',  ( -0.4453226528549816265, -2.225540348348185052E-17, 2.000000000000000000 ) ) ;
#11471=CARTESIAN_POINT ( 'NONE',  ( -3.054861441201806915, -2.473751543679003184, -1.000000000000011768 ) ) ;
#11484=EDGE_LOOP ( 'NONE', ( #14508, #190, #2409, #7996 ) ) ;
#11486=CARTESIAN_POINT ( 'NONE',  ( -2.837468109123414628, -2.529993217055221510, -0.7946808062269109518 ) ) ;
#11495=PLANE ( 'NONE',  #1034 ) ;
#11508=DIRECTION ( 'NONE',  ( 0.000000000000000000, 0.000000000000000000, 1.000000000000000000 ) ) ;
#11513=ORIENTED_EDGE ( 'NONE', *, *, #6499, .F. ) ;
#11529=CLOSED_SHELL ( 'NONE', ( #7699, #8655, #7678, #8755, #9513, #14914, #8057, #6563, #12152, #11186, #8833, #6783, #2436, #2912, #3567, #4516, #10077, #433, #7589, #5088, #5518 ) ) ;
#11568=EDGE_CURVE ( 'NONE', #10459, #10124, #1521, .T. ) ;
#11598=CARTESIAN_POINT ( 'NONE',  ( 1.052436484934203831, 2.165641995257063801, -1.000000000000007772 ) ) ;
#11628=CIRCLE ( 'NONE', #4470, 1.000000000000000000 ) ;
#11684=ORIENTED_EDGE ( 'NONE', *, *, #5789, .T. ) ;
#11702=ORIENTED_EDGE ( 'NONE', *, *, #8776, .T. ) ;
#11703=CARTESIAN_POINT ( 'NONE',  ( 3.035840392568594837, -0.9800309627322405515, -1.000000000000001110 ) ) ;
#11715=FACE_BOUND ( 'NONE', #7877, .T. ) ;
#11721=CARTESIAN_POINT ( 'NONE',  ( -10.29275726619092524, 0.000000000000000000, -34.56909192082969184 ) ) ;
#11744=CARTESIAN_POINT ( 'NONE',  ( 7.148068729939690336, -2.490287375297125294, -34.56909192082981974 ) ) ;
#11786=DIRECTION ( 'NONE',  ( 1.000000000000000000, 0.000000000000000000, -0.000000000000000000 ) ) ;
#11789=CARTESIAN_POINT ( 'NONE',  ( 2.548347919319509103, 1.829703814864835465, -1.000000000000001110 ) ) ;
#11792=CARTESIAN_POINT ( 'NONE',  ( 7.148068729939690336, 2.490287375297125294, -34.56909192082981974 ) ) ;
#11796=CARTESIAN_POINT ( 'NONE',  ( -4.507264730511037598, -1.628626824712336107, -1.000000000000001332 ) ) ;
#11808=ORIENTED_EDGE ( 'NONE', *, *, #12628, .F. ) ;
#11855=VECTOR ( 'NONE', #3125, 1000.000000000000114 ) ;
#11863=CARTESIAN_POINT ( 'NONE',  ( 3.158384440324536691, 0.000000000000000000, -1.000000000000001332 ) ) ;
#11897=TOROIDAL_SURFACE ( 'NONE', #10470, 4.000000000000000000, 1.000000000000000000 ) ;
#11908=CARTESIAN_POINT ( 'NONE',  ( -0.8336906130587268260, -1.921202954650397032, -45.08225561976305329 ) ) ;
#11911=CYLINDRICAL_SURFACE ( 'NONE', #2558, 7.428243039713066764 ) ;
#11986=CARTESIAN_POINT ( 'NONE',  ( -9.742503157198443731, -2.490287375297126626, -40.35209559314896666 ) ) ;
#11989=DIRECTION ( 'NONE',  ( 0.1564344650402314796, 0.000000000000000000, 0.9876883405951375483 ) ) ;
#12015=CARTESIAN_POINT ( 'NONE',  ( -9.030574454602197321, 2.490287375297123962, -34.97919997656152447 ) ) ;
#12031=CARTESIAN_POINT ( 'NONE',  ( -8.671560925439079526, 2.743867526398026779, -35.09585054340070798 ) ) ;
#12062=CARTESIAN_POINT ( 'NONE',  ( -0.9087754948914894548, 0.000000000000000000, -45.55632290616385660 ) ) ;
#12105=DIRECTION ( 'NONE',  ( 0.000000000000000000, 0.000000000000000000, 1.000000000000000000 ) ) ;
#12117=VERTEX_POINT ( 'NONE', #3113 ) ;
#12149=ORIENTED_EDGE ( 'NONE', *, *, #5347, .F. ) ;
#12152=ADVANCED_FACE ( 'NONE', ( #575 ), #10149, .F. ) ;
#12166=EDGE_LOOP ( 'NONE', ( #5928, #12624, #10547, #12857 ) ) ;
#12204=CARTESIAN_POINT ( 'NONE',  ( 7.148068729939693000, 2.490287375297123962, -34.56909192082981974 ) ) ;
#12266=CARTESIAN_POINT ( 'NONE',  ( -9.030574454602195544, -2.490287375297124850, -34.97919997656152447 ) ) ;
#12307=CARTESIAN_POINT ( 'NONE',  ( -0.5793326530874192137, 2.529993217055222843, -43.47630266472464911 ) ) ;
#12310=DIRECTION ( 'NONE',  ( 0.000000000000000000, 0.000000000000000000, 1.000000000000000000 ) ) ;
#12318=ORIENTED_EDGE ( 'NONE', *, *, #2158, .T. ) ;
#12358=AXIS2_PLACEMENT_3D ( 'NONE', #14288, #9645, #2384 ) ;
#12372=ORIENTED_EDGE ( 'NONE', *, *, #4765, .F. ) ;
#12378=DIRECTION ( 'NONE',  ( 0.000000000000000000, 0.000000000000000000, -1.000000000000000000 ) ) ;
#12385=CARTESIAN_POINT ( 'NONE',  ( -9.742503157198449060, 2.490287375297123962, -40.35209559314896666 ) ) ;
#12403=LINE ( 'NONE', #820, #10639 ) ;
#12406=AXIS2_PLACEMENT_3D ( 'NONE', #5566, #3325, #12678 ) ;
#12423=EDGE_LOOP ( 'NONE', ( #13528, #12851, #12372, #5807 ) ) ;
#12427=DIRECTION ( 'NONE',  ( 0.000000000000000000, 1.000000000000000000, 0.000000000000000000 ) ) ;
#12432=CYLINDRICAL_SURFACE ( 'NONE', #4540, 5.000000000000000000 ) ;
#12489=CARTESIAN_POINT ( 'NONE',  ( -2.837468109123414628, -2.075239479414269894, -0.7946808062269106188 ) ) ;
#12500=CARTESIAN_POINT ( 'NONE',  ( -4.038200276543141953, 2.192442743657398552, -1.000000000000011768 ) ) ;
#12515=DIRECTION ( 'NONE',  ( -0.000000000000000000, -1.000000000000000000, -0.000000000000000000 ) ) ;
#12516=CARTESIAN_POINT ( 'NONE',  ( 8.131300352726233527, -2.490287375297125294, -39.89901737624450107 ) ) ;
#12540=DIRECTION ( 'NONE',  ( -0.9876883405951376593, 0.000000000000000000, 0.1564344650402315073 ) ) ;
#12596=CARTESIAN_POINT ( 'NONE',  ( 6.369258321017760238, -2.075239479414269894, -34.56909192082981974 ) ) ;
#12602=CARTESIAN_POINT ( 'NONE',  ( 1.667634992416483941, -2.570071824251322301, -1.000000000000001776 ) ) ;
#12603=CARTESIAN_POINT ( 'NONE',  ( 7.995229681650334541, -1.921202954650395700, -34.56909192082981974 ) ) ;
#12604=AXIS2_PLACEMENT_3D ( 'NONE', #11277, #7567, #8732 ) ;
#12614=CARTESIAN_POINT ( 'NONE',  ( 1.052436484934203387, 2.075239479414269894, -1.000000000000007772 ) ) ;
#12623=EDGE_CURVE ( 'NONE', #10124, #2052, #10170, .T. ) ;
#12624=ORIENTED_EDGE ( 'NONE', *, *, #9328, .T. ) ;
#12628=EDGE_CURVE ( 'NONE', #13029, #14984, #1349, .T. ) ;
#12639=DIRECTION ( 'NONE',  ( -0.1564344650402312298, -0.000000000000000000, 0.9876883405951376593 ) ) ;
#12645=CARTESIAN_POINT ( 'NONE',  ( -3.578160823487106956, -2.490287375297124406, -0.5540151544739178036 ) ) ;
#12657=( BOUNDED_SURFACE ( )  B_SPLINE_SURFACE ( 3, 1, ( 
 ( #7927, #12489 ),
 ( #5677, #11486 ),
 ( #5381, #5531 ),
 ( #3208, #12645 ) ),
 .UNSPECIFIED., .F., .F., .F. ) 
 B_SPLINE_SURFACE_WITH_KNOTS ( ( 4, 4 ),
 ( 2, 2 ),
 ( 0.000000000000000000, 1.000000000000000000 ),
 ( 0.000000000000000000, 1.000000000000000000 ),
 .UNSPECIFIED. ) 
 GEOMETRIC_REPRESENTATION_ITEM ( )  RATIONAL_B_SPLINE_SURFACE ( (
 ( 1.000000000000000000, 1.000000000000000000),
 ( 0.6468719831415916666, 0.6468719831415916666),
 ( 0.6468719831415916666, 0.6468719831415916666),
 ( 1.000000000000000000, 1.000000000000000000) ) ) 
 REPRESENTATION_ITEM ( '' )  SURFACE ( )  );
#12678=DIRECTION ( 'NONE',  ( 1.000000000000000000, 0.000000000000000000, 0.000000000000000000 ) ) ;
#12763=LINE ( 'NONE', #3479, #13178 ) ;
#12826=ORIENTED_EDGE ( 'NONE', *, *, #14252, .T. ) ;
#12843=CARTESIAN_POINT ( 'NONE',  ( 1.238244973495889356, 2.474488745542209767, -1.000000000000001332 ) ) ;
#12851=ORIENTED_EDGE ( 'NONE', *, *, #2158, .F. ) ;
#12857=ORIENTED_EDGE ( 'NONE', *, *, #1384, .F. ) ;
#12861=CARTESIAN_POINT ( 'NONE',  ( -2.869987474717051068, -2.075239479414269894, -1.000000000000004441 ) ) ;
#12891=ORIENTED_EDGE ( 'NONE', *, *, #14636, .T. ) ;
#12894=CARTESIAN_POINT ( 'NONE',  ( 8.978461304436878621, 1.921202954650395478, -40.45944830867332342 ) ) ;
#12909=VERTEX_POINT ( 'NONE', #6293 ) ;
#12925=EDGE_CURVE ( 'NONE', #8581, #9140, #11375, .T. ) ;
#12938=EDGE_LOOP ( 'NONE', ( #8527, #11421, #4381, #203 ) ) ;
#12943=DIRECTION ( 'NONE',  ( 1.000000000000000000, 0.000000000000000000, 0.000000000000000000 ) ) ;
#12963=CARTESIAN_POINT ( 'NONE',  ( -9.742503157198443731, -2.490287375297125294, -40.35209559314896666 ) ) ;
#12970=CARTESIAN_POINT ( 'NONE',  ( 9.458437899194636955, 0.000000000000000000, -40.77697206847473410 ) ) ;
#12985=VERTEX_POINT ( 'NONE', #6214 ) ;
#12994=DIRECTION ( 'NONE',  ( 0.000000000000000000, 0.000000000000000000, 1.000000000000000000 ) ) ;
#13021=EDGE_LOOP ( 'NONE', ( #10191, #4669, #10177, #6969 ) ) ;
#13029=VERTEX_POINT ( 'NONE', #11157 ) ;
#13037=CARTESIAN_POINT ( 'NONE',  ( 3.158384440324535802, 0.2459835157955773399, -1.000000000000001110 ) ) ;
#13056=( BOUNDED_SURFACE ( )  B_SPLINE_SURFACE ( 3, 3, ( 
 ( #407, #7272, #9831, #2491, #329, #11986, #1409 ),
 ( #5196, #9910, #14406, #11908, #8509, #173, #245 ),
 ( #1333, #2571, #10991, #5042, #10827, #8585, #4880 ),
 ( #6036, #13244, #2647, #12062, #1480, #6195, #14488 ) ),
 .UNSPECIFIED., .F., .F., .F. ) 
 B_SPLINE_SURFACE_WITH_KNOTS ( ( 4, 4 ),
 ( 4, 3, 4 ),
 ( 0.000000000000000000, 1.000000000000000000 ),
 ( 0.000000000000000000, 0.5000000000000000000, 1.000000000000000000 ),
 .UNSPECIFIED. ) 
 GEOMETRIC_REPRESENTATION_ITEM ( )  RATIONAL_B_SPLINE_SURFACE ( (
 ( 1.000000000000000000, 0.7662986988867873661, 0.7662986988867873661, 1.000000000000000000, 0.7662986988867873661, 0.7662986988867873661, 1.000000000000000000),
 ( 0.9216682375510407699, 0.7062731712406410400, 0.7062731712406410400, 0.9216682375510407699, 0.7062731712406410400, 0.7062731712406410400, 0.9216682375510407699),
 ( 0.9216682375510407699, 0.7062731712406410400, 0.7062731712406410400, 0.9216682375510407699, 0.7062731712406410400, 0.7062731712406410400, 0.9216682375510407699),
 ( 1.000000000000000000, 0.7662986988867873661, 0.7662986988867873661, 1.000000000000000000, 0.7662986988867873661, 0.7662986988867873661, 1.000000000000000000) ) ) 
 REPRESENTATION_ITEM ( '' )  SURFACE ( )  );
#13079=CARTESIAN_POINT ( 'NONE',  ( -4.445322652854981627, 4.676033161754593892E-16, 1.000000000000000000 ) ) ;
#13087=CIRCLE ( 'NONE', #2474, 2.999999999999999112 ) ;
#13165=CARTESIAN_POINT ( 'NONE',  ( -9.030574454602197321, 2.490287375297123962, -34.97919997656152447 ) ) ;
#13178=VECTOR ( 'NONE', #13850, 1000.000000000000000 ) ;
#13244=CARTESIAN_POINT ( 'NONE',  ( 9.458437899194636955, 0.000000000000000000, -40.77697206847473410 ) ) ;
#13273=CARTESIAN_POINT ( 'NONE',  ( 4.554677347145018373, -2.225540348348185052E-17, -1.000000000000000000 ) ) ;
#13290=LINE ( 'NONE', #299, #9395 ) ;
#13309=DIRECTION ( 'NONE',  ( 0.000000000000000000, 0.000000000000000000, 1.000000000000000000 ) ) ;
#13321=DIRECTION ( 'NONE',  ( 0.000000000000000000, 0.000000000000000000, 1.000000000000000000 ) ) ;
#13329=CARTESIAN_POINT ( 'NONE',  ( 7.148068729939693000, 2.490287375297123518, -34.56909192082981974 ) ) ;
#13334=FACE_OUTER_BOUND ( 'NONE', #15197, .T. ) ;
#13389=CARTESIAN_POINT ( 'NONE',  ( 6.369258321017760238, -2.529993217055220178, -34.56909192082981974 ) ) ;
#13429=ORIENTED_EDGE ( 'NONE', *, *, #4220, .T. ) ;
#13432=DIRECTION ( 'NONE',  ( 0.000000000000000000, 0.000000000000000000, 1.000000000000000000 ) ) ;
#13489=CARTESIAN_POINT ( 'NONE',  ( -7.439587717305479408, 0.000000000000000000, -35.49614290395457772 ) ) ;
#13519=CARTESIAN_POINT ( 'NONE',  ( -10.29275726619092524, -1.020558061026469066, -34.56909192082969184 ) ) ;
#13528=ORIENTED_EDGE ( 'NONE', *, *, #5451, .F. ) ;
#13574=CARTESIAN_POINT ( 'NONE',  ( -2.869987474717192732, -2.165641995260736863, -0.9999999999968022246 ) ) ;
#13589=VECTOR ( 'NONE', #12639, 1000.000000000000114 ) ;
#13596=EDGE_CURVE ( 'NONE', #4779, #12117, #14099, .T. ) ;
#13602=CIRCLE ( 'NONE', #1984, 3.000000000000000000 ) ;
#13637=FACE_OUTER_BOUND ( 'NONE', #13021, .T. ) ;
#13652=B_SPLINE_CURVE_WITH_KNOTS ( 'NONE', 3,
 ( #13771, #9198, #12602, #15173, #4566, #5638, #2093, #10512, #9348, #15017 ),
 .UNSPECIFIED., .F., .F.,
 ( 4, 2, 2, 2, 4 ),
 ( 9.697399036122160616E-19, 0.0002702708960404995829, 0.0005405417920809981900, 0.0008108126881214967972, 0.001081083584161995296 ),
 .UNSPECIFIED. ) ;
#13666=EDGE_CURVE ( 'NONE', #8297, #13794, #769, .T. ) ;
#13701=CARTESIAN_POINT ( 'NONE',  ( -0.4453226528549816265, -2.225540348348185052E-17, 1.000000000000000000 ) ) ;
#13726=LINE ( 'NONE', #1821, #11855 ) ;
#13765=ORIENTED_EDGE ( 'NONE', *, *, #5789, .F. ) ;
#13771=CARTESIAN_POINT ( 'NONE',  ( 1.831246893856133928, -2.490287375297125294, -1.000000000000000888 ) ) ;
#13780=CARTESIAN_POINT ( 'NONE',  ( 1.397354133952893873, 2.559042896907057774, -1.000000000000001332 ) ) ;
#13782=EDGE_CURVE ( 'NONE', #3650, #13806, #6449, .T. ) ;
#13794=VERTEX_POINT ( 'NONE', #12015 ) ;
#13806=VERTEX_POINT ( 'NONE', #13273 ) ;
#13843=ORIENTED_EDGE ( 'NONE', *, *, #10056, .T. ) ;
#13847=AXIS2_PLACEMENT_3D ( 'NONE', #8061, #10604, #7048 ) ;
#13850=DIRECTION ( 'NONE',  ( 0.000000000000000000, 0.000000000000000000, 1.000000000000000000 ) ) ;
#13857=CIRCLE ( 'NONE', #7433, 0.4999999999999995559 ) ;
#13875=EDGE_CURVE ( 'NONE', #1578, #9311, #12403, .T. ) ;
#13877=CARTESIAN_POINT ( 'NONE',  ( -3.485185982199345389, -2.570071824251316084, -1.000000000000001332 ) ) ;
#13911=AXIS2_PLACEMENT_3D ( 'NONE', #4160, #7383, #12105 ) ;
#13936=CARTESIAN_POINT ( 'NONE',  ( 6.369258321017759350, -2.075239479414269894, -34.56909192082981974 ) ) ;
#13977=( BOUNDED_SURFACE ( )  B_SPLINE_SURFACE ( 3, 3, ( 
 ( #8313, #12970, #8469, #3766, #4766, #2607, #1207 ),
 ( #1066, #7144, #7072, #9554, #8241, #14133, #5774 ),
 ( #14279, #12894, #3609, #1141, #15299, #3679, #5844 ),
 ( #11792, #4691, #9408, #8389, #14053, #5915, #3531 ) ),
 .UNSPECIFIED., .F., .F., .F. ) 
 B_SPLINE_SURFACE_WITH_KNOTS ( ( 4, 4 ),
 ( 4, 3, 4 ),
 ( 0.000000000000000000, 1.000000000000000000 ),
 ( 0.000000000000000000, 0.5000000000000000000, 1.000000000000000000 ),
 .UNSPECIFIED. ) 
 GEOMETRIC_REPRESENTATION_ITEM ( )  RATIONAL_B_SPLINE_SURFACE ( (
 ( 1.000000000000000000, 0.7662986988867873661, 0.7662986988867873661, 1.000000000000000000, 0.7662986988867873661, 0.7662986988867873661, 1.000000000000000000),
 ( 0.9216682375510407699, 0.7062731712406410400, 0.7062731712406410400, 0.9216682375510407699, 0.7062731712406410400, 0.7062731712406410400, 0.9216682375510407699),
 ( 0.9216682375510407699, 0.7062731712406410400, 0.7062731712406410400, 0.9216682375510407699, 0.7062731712406410400, 0.7062731712406410400, 0.9216682375510407699),
 ( 1.000000000000000000, 0.7662986988867873661, 0.7662986988867873661, 1.000000000000000000, 0.7662986988867873661, 0.7662986988867873661, 1.000000000000000000) ) ) 
 REPRESENTATION_ITEM ( '' )  SURFACE ( )  );
#13980=EDGE_CURVE ( 'NONE', #12909, #8581, #11628, .T. ) ;
#14009=VECTOR ( 'NONE', #14740, 1000.000000000000000 ) ;
#14035=EDGE_LOOP ( 'NONE', ( #2495, #15050, #4247, #9237 ) ) ;
#14049=CARTESIAN_POINT ( 'NONE',  ( 1.831246893856137481, 2.490287375297123074, -1.000000000000007772 ) ) ;
#14053=CARTESIAN_POINT ( 'NONE',  ( -6.119281984250456219, 2.490287375297125294, -44.38286699775952826 ) ) ;
#14099=CIRCLE ( 'NONE', #4463, 7.428243039713066764 ) ;
#14121=PRODUCT ( 'ShearsLockingLatch_Predeterminado', 'ShearsLockingLatch_Predeterminado', '', ( #380 ) ) ;
#14133=CARTESIAN_POINT ( 'NONE',  ( -11.27598888897756702, 1.020558061026469510, -40.77697206847461331 ) ) ;
#14137=DIRECTION ( 'NONE',  ( 1.000000000000000000, 0.000000000000000000, 0.000000000000000000 ) ) ;
#14153=( BOUNDED_SURFACE ( )  B_SPLINE_SURFACE ( 3, 3, ( 
 ( #11209, #630, #1551, #14554, #3951, #5335, #8654 ),
 ( #13389, #2793, #6342, #9897, #10630, #7803, #15293 ),
 ( #4683, #1932, #6721, #9399, #2297, #3089, #8235 ),
 ( #5909, #12516, #3444, #2009, #1202, #12963, #51 ) ),
 .UNSPECIFIED., .F., .F., .T. ) 
 B_SPLINE_SURFACE_WITH_KNOTS ( ( 4, 4 ),
 ( 4, 3, 4 ),
 ( 0.000000000000000000, 1.000000000000000000 ),
 ( 0.000000000000000000, 0.5000000000000000000, 1.000000000000000000 ),
 .UNSPECIFIED. ) 
 GEOMETRIC_REPRESENTATION_ITEM ( )  RATIONAL_B_SPLINE_SURFACE ( (
 ( 1.000000000000000000, 0.7662986988867873661, 0.7662986988867873661, 1.000000000000000000, 0.7662986988867873661, 0.7662986988867873661, 1.000000000000000000),
 ( 0.6468719831415924437, 0.4956971590277181594, 0.4956971590277181594, 0.6468719831415924437, 0.4956971590277181594, 0.4956971590277181594, 0.6468719831415924437),
 ( 0.6468719831415924437, 0.4956971590277181594, 0.4956971590277181594, 0.6468719831415924437, 0.4956971590277181594, 0.4956971590277181594, 0.6468719831415924437),
 ( 1.000000000000000000, 0.7662986988867873661, 0.7662986988867873661, 1.000000000000000000, 0.7662986988867873661, 0.7662986988867873661, 1.000000000000000000) ) ) 
 REPRESENTATION_ITEM ( '' )  SURFACE ( )  );
#14232=CARTESIAN_POINT ( 'NONE',  ( 5.475206276408092876, 0.000000000000000000, -34.56909192082981974 ) ) ;
#14252=EDGE_CURVE ( 'NONE', #6217, #5312, #5946, .T. ) ;
#14279=CARTESIAN_POINT ( 'NONE',  ( 7.995229681650334541, 1.921202954650395700, -34.56909192082981974 ) ) ;
#14288=CARTESIAN_POINT ( 'NONE',  ( -0.4453226528549816265, -2.225540348348185052E-17, 1.000000000000000000 ) ) ;
#14343=ORIENTED_EDGE ( 'NONE', *, *, #8346, .T. ) ;
#14352=VECTOR ( 'NONE', #8741, 1000.000000000000227 ) ;
#14368=( GEOMETRIC_REPRESENTATION_CONTEXT ( 3 ) GLOBAL_UNCERTAINTY_ASSIGNED_CONTEXT ( ( #634 ) ) GLOBAL_UNIT_ASSIGNED_CONTEXT ( ( #8357, #8595, #9603 ) ) REPRESENTATION_CONTEXT ( 'NONE', 'WORKASPACE' ) );
#14406=CARTESIAN_POINT ( 'NONE',  ( 5.137957026085648415, -1.921202954650397476, -45.03258396026099319 ) ) ;
#14425=VECTOR ( 'NONE', #11989, 1000.000000000000227 ) ;
#14445=EDGE_CURVE ( 'NONE', #13806, #3650, #9899, .T. ) ;
#14488=CARTESIAN_POINT ( 'NONE',  ( -10.29275726619094300, 0.000000000000000000, -34.56909192082969895 ) ) ;
#14507=EDGE_CURVE ( 'NONE', #14984, #9311, #4411, .T. ) ;
#14508=ORIENTED_EDGE ( 'NONE', *, *, #4694, .F. ) ;
#14554=CARTESIAN_POINT ( 'NONE',  ( -0.5793326530874193248, -2.075239479414269894, -43.47630266472464911 ) ) ;
#14577=CARTESIAN_POINT ( 'NONE',  ( 1.831246893856141034, 2.490287375297123962, -1.000000000000028644 ) ) ;
#14578=ORIENTED_EDGE ( 'NONE', *, *, #13875, .T. ) ;
#14581=PLANE ( 'NONE',  #3950 ) ;
#14592=VECTOR ( 'NONE', #10921, 1000.000000000000227 ) ;
#14606=CARTESIAN_POINT ( 'NONE',  ( -9.836272398077403167, -1.921202954650395478, -34.71741284551207229 ) ) ;
#14636=EDGE_CURVE ( 'NONE', #4779, #6217, #13857, .T. ) ;
#14665=CIRCLE ( 'NONE', #13911, 7.428243039713066764 ) ;
#14683=CARTESIAN_POINT ( 'NONE',  ( -4.878690035801932723, -1.020558061026469066, -0.3860167444088121180 ) ) ;
#14691=CARTESIAN_POINT ( 'NONE',  ( -3.219147294324499420, 2.743867526398026779, -0.6706657213163130793 ) ) ;
#14707=CARTESIAN_POINT ( 'NONE',  ( -3.486358512013132849, 2.569799602646718917, -1.000000000000001110 ) ) ;
#14733=CARTESIAN_POINT ( 'NONE',  ( -6.119281984250459772, 2.490287375297123962, -44.38286699775954247 ) ) ;
#14740=DIRECTION ( 'NONE',  ( 0.000000000000000000, 1.000000000000000000, 0.000000000000000000 ) ) ;
#14750=CARTESIAN_POINT ( 'NONE',  ( -3.573755135672850081, -2.540697700116522739, -1.000000000000004663 ) ) ;
#14804=CARTESIAN_POINT ( 'NONE',  ( 1.831246893856141034, 2.490287375297123518, -1.000000000000028644 ) ) ;
#14823=DIRECTION ( 'NONE',  ( 0.1564344650402314796, 0.000000000000000000, 0.9876883405951375483 ) ) ;
#14882=CARTESIAN_POINT ( 'NONE',  ( 6.369258321017759350, 2.529993217055222843, -34.56909192082981974 ) ) ;
#14914=ADVANCED_FACE ( 'NONE', ( #10412, #2069, #11715 ), #11495, .F. ) ;
#14935=CARTESIAN_POINT ( 'NONE',  ( -0.4453226528549816265, -2.225540348348185052E-17, -1.000000000000000000 ) ) ;
#14971=ORIENTED_EDGE ( 'NONE', *, *, #10056, .F. ) ;
#14984=VERTEX_POINT ( 'NONE', #4613 ) ;
#14992=EDGE_LOOP ( 'NONE', ( #11684, #9501, #3427, #8427 ) ) ;
#15016=ORIENTED_EDGE ( 'NONE', *, *, #4424, .F. ) ;
#15017=CARTESIAN_POINT ( 'NONE',  ( 1.052436484934202499, -2.075239479414269894, -1.000000000000000888 ) ) ;
#15028=CARTESIAN_POINT ( 'NONE',  ( -8.765409998386077817, 2.075239479414269450, -35.06535713112702979 ) ) ;
#15044=CARTESIAN_POINT ( 'NONE',  ( -2.869987474717050624, 2.075239479414269894, -1.000000000000000888 ) ) ;
#15050=ORIENTED_EDGE ( 'NONE', *, *, #4694, .T. ) ;
#15068=CARTESIAN_POINT ( 'NONE',  ( -4.827512413385830037, 0.9636447990543512976, -1.000000000000001332 ) ) ;
#15070=EDGE_LOOP ( 'NONE', ( #8937, #13843, #3285, #8533 ) ) ;
#15088=CARTESIAN_POINT ( 'NONE',  ( 1.831246893856136593, -2.490287375297125294, -1.000000000000021760 ) ) ;
#15105=AXIS2_PLACEMENT_3D ( 'NONE', #14935, #11508, #11349 ) ;
#15133=EDGE_LOOP ( 'NONE', ( #5367, #9596, #11326, #8301 ) ) ;
#15173=CARTESIAN_POINT ( 'NONE',  ( 1.487533013587992059, -2.579141538380385956, -1.000000000000001110 ) ) ;
#15182=DIRECTION ( 'NONE',  ( -0.3090169943749621062, 0.000000000000000000, -0.9510565162951489793 ) ) ;
#15197=EDGE_LOOP ( 'NONE', ( #8029, #267, #7424, #10093 ) ) ;
#15234=CARTESIAN_POINT ( 'NONE',  ( -4.853391382351440519, -0.9800309627322401074, -1.000000000000001110 ) ) ;
#15245=EDGE_LOOP ( 'NONE', ( #14971, #2300, #2883, #4764 ) ) ;
#15272=CARTESIAN_POINT ( 'NONE',  ( 0.000000000000000000, 0.000000000000000000, 0.000000000000000000 ) ) ;
#15293=CARTESIAN_POINT ( 'NONE',  ( -8.289881740238515206, -2.529993217055220178, -35.21986562831452261 ) ) ;
#15299=CARTESIAN_POINT ( 'NONE',  ( -6.805338252203106286, 1.921202954650395478, -45.13192727926512759 ) ) ;
#15332=COLOUR_RGB('Light Blue', 0.31764706, 0.68627451, 0.89019608);
#15333=FILL_AREA_STYLE_COLOUR('',#15332);
#15334=FILL_AREA_STYLE('',(#15333));
#15335=SURFACE_STYLE_FILL_AREA(#15334);
#15336=SURFACE_SIDE_STYLE('',(#15335));
#15337=SURFACE_STYLE_USAGE(.BOTH.,#15336);
#15338=PRESENTATION_STYLE_ASSIGNMENT((#15337));
#15373=STYLED_ITEM('',(#15338),#2311);
#15374=MECHANICAL_DESIGN_GEOMETRIC_PRESENTATION_REPRESENTATION('',(#15373),#14368);
ENDSEC;
END-ISO-10303-21;
